ISO-10303-21;
HEADER;
FILE_DESCRIPTION (('STEP AP214'),
    '1' );
FILE_NAME ('Nut M6.step',
    '2026-10-06T09:00:30',
    ( '' ),
    ( '' ),
    'SwSTEP 2.0',
    'SolidWorks 2020',
    '' );
FILE_SCHEMA (( 'AUTOMOTIVE_DESIGN' ));
ENDSEC;

DATA;
#48=CARTESIAN_POINT ( 'NONE',  ( -12.32027642597168260, -32.00000000000000711, -27.84664838113162233 ) ) ;
#71=VECTOR ( 'NONE', #9226, 1000.000000000000000 ) ;
#205=ORIENTED_EDGE ( 'NONE', *, *, #16530, .T. ) ;
#265=CARTESIAN_POINT ( 'NONE',  ( -17.49268987146206555, -21.99976866032092460, -27.95151664070907316 ) ) ;
#277=CONICAL_SURFACE ( 'NONE', #23882, 4.987531172069999741, 1.047197551199999799 ) ;
#296=CARTESIAN_POINT ( 'NONE',  ( -17.49199711315135986, -24.60220466956999985, -24.01086508779000184 ) ) ;
#340=CARTESIAN_POINT ( 'NONE',  ( -12.38103409318611270, -30.48833240864483685, -24.64074601757454630 ) ) ;
#350=PRESENTATION_STYLE_ASSIGNMENT (( #5052 ) ) ;
#361=CARTESIAN_POINT ( 'NONE',  ( -12.41750254862020952, -32.00000000000000711, -29.79893583387511669 ) ) ;
#363=FACE_OUTER_BOUND ( 'NONE', #1822, .T. ) ;
#377=CARTESIAN_POINT ( 'NONE',  ( -17.39952085737849075, -31.99978942475004118, -27.11779176627238641 ) ) ;
#386=CARTESIAN_POINT ( 'NONE',  ( -12.34929264641464464, -28.75102117903383458, -33.16229187319683547 ) ) ;
#396=CARTESIAN_POINT ( 'NONE',  ( -12.32161713220065735, -24.97215432380749434, -23.79754533132837935 ) ) ;
#525=ORIENTED_EDGE ( 'NONE', *, *, #2715, .F. ) ;
#536=CARTESIAN_POINT ( 'NONE',  ( -17.19097361925006595, -31.99975500943657281, -30.75789318072767742 ) ) ;
#548=FACE_OUTER_BOUND ( 'NONE', #11882, .T. ) ;
#590=COLOUR_RGB ( '', 0.09019608, 0.27058824, 0.51372549) ;
#646=CARTESIAN_POINT ( 'NONE',  ( -12.39443769393950845, -30.57364707460137510, -24.68998539662501557 ) ) ;
#664=CARTESIAN_POINT ( 'NONE',  ( -12.44217317844253756, -31.99999999999999289, -29.95172824868416583 ) ) ;
#666=CARTESIAN_POINT ( 'NONE',  ( -14.89999999969999855, -27.00000000000000000, -28.40000000020000215 ) ) ;
#683=CARTESIAN_POINT ( 'NONE',  ( -17.12355120911804462, -32.00000000000027001, -31.01886516981582886 ) ) ;
#765=CARTESIAN_POINT ( 'NONE',  ( -12.41345480022557446, -25.68646278880473233, -33.41489075299887901 ) ) ;
#796=CARTESIAN_POINT ( 'NONE',  ( -12.41832131460176392, -28.28617032314356905, -23.36932019586331677 ) ) ;
#814=ORIENTED_EDGE ( 'NONE', *, *, #9548, .T. ) ;
#872=UNCERTAINTY_MEASURE_WITH_UNIT (LENGTH_MEASURE( 1.000000000000000082E-05 ), #5198, 'distance_accuracy_value', 'NONE');
#944=ORIENTED_EDGE ( 'NONE', *, *, #20701, .T. ) ;
#985=EDGE_CURVE ( 'NONE', #14751, #26486, #21786, .T. ) ;
#1013=( NAMED_UNIT ( * ) SI_UNIT ( $, .STERADIAN. ) SOLID_ANGLE_UNIT ( ) );
#1059=CARTESIAN_POINT ( 'NONE',  ( -17.22797207741465897, -26.41666101526536892, -33.83671177223448012 ) ) ;
#1068=DIRECTION ( 'NONE',  ( 0.000000000000000000, 0.5000000000001900702, -0.8660254037843290176 ) ) ;
#1122=ORIENTED_EDGE ( 'NONE', *, *, #9649, .F. ) ;
#1159=( NAMED_UNIT ( * ) PLANE_ANGLE_UNIT ( ) SI_UNIT ( $, .RADIAN. ) );
#1213=CARTESIAN_POINT ( 'NONE',  ( -12.29999999976166158, -29.62135916506277411, -29.91085694131270500 ) ) ;
#1219=ORIENTED_EDGE ( 'NONE', *, *, #2519, .F. ) ;
#1328=B_SPLINE_CURVE_WITH_KNOTS ( 'NONE', 3,
 ( #10500, #17710, #18187, #1213, #1368, #3401, #22303, #20101, #15370, #24967, #6075, #20239, #13005, #8423, #20558, #29837, #8272, #27472 ),
 .UNSPECIFIED., .F., .F.,
 ( 4, 2, 2, 2, 2, 2, 2, 2, 4 ),
 ( 0.000000000000000000, 0.1249999999999997224, 0.2499999999999994449, 0.3749999999999991673, 0.4999999999999993339, 0.6249999999999994449, 0.7499999999999996669, 0.8749999999999997780, 1.000000000000000000 ),
 .UNSPECIFIED. ) ;
#1368=CARTESIAN_POINT ( 'NONE',  ( -12.29999999977708214, -29.39900052719453782, -30.24364016012474465 ) ) ;
#1382=FACE_OUTER_BOUND ( 'NONE', #9321, .T. ) ;
#1475=VERTEX_POINT ( 'NONE', #25437 ) ;
#1491=DIRECTION ( 'NONE',  ( 0.4999999999969509945, -0.4151946956549595336, -0.7600087925169251024 ) ) ;
#1492=CARTESIAN_POINT ( 'NONE',  ( -17.46645031549676830, -23.90523224175912631, -24.41319780928835925 ) ) ;
#1551=B_SPLINE_CURVE_WITH_KNOTS ( 'NONE', 3,
 ( #19893, #12485, #396, #24610, #20036, #5403, #7910, #29163, #15157, #22098, #7610, #7761, #2743, #10594 ),
 .UNSPECIFIED., .F., .F.,
 ( 4, 2, 2, 1, 1, 2, 2, 4 ),
 ( 0.000000000000000000, 0.2500000000000100475, 0.3750000000000123790, 0.4375000000000153211, 0.4687500000000160427, 0.4843750000000174305, 0.5000000000000187628, 1.000000000000000000 ),
 .UNSPECIFIED. ) ;
#1566=CARTESIAN_POINT ( 'NONE',  ( -17.47972357343302363, -29.97921655931956764, -24.34654879079820233 ) ) ;
#1593=VERTEX_POINT ( 'NONE', #5679 ) ;
#1623=FACE_OUTER_BOUND ( 'NONE', #6376, .T. ) ;
#1719=CARTESIAN_POINT ( 'NONE',  ( -17.31982526421591828, -31.07774283049385033, -24.98078322917286442 ) ) ;
#1822=EDGE_LOOP ( 'NONE', ( #6644, #944, #26325, #17336 ) ) ;
#1840=CARTESIAN_POINT ( 'NONE',  ( -12.38084235052671822, -22.00000000000000355, -29.54157481573779975 ) ) ;
#1865=VERTEX_POINT ( 'NONE', #20050 ) ;
#1886=CARTESIAN_POINT ( 'NONE',  ( -17.47315945020183037, -28.94086986751210588, -33.05294095162887658 ) ) ;
#1942=B_SPLINE_CURVE_WITH_KNOTS ( 'NONE', 3,
 ( #1979, #9825, #26502, #2126, #30923, #21476, #4945, #17056, #14556, #26049, #14240 ),
 .UNSPECIFIED., .F., .F.,
 ( 4, 1, 1, 1, 2, 2, 4 ),
 ( 0.000000000000000000, 0.2500000000000019429, 0.3750000000000003886, 0.4375000000000022204, 0.4687500000000021649, 0.5000000000000019984, 1.000000000000000000 ),
 .UNSPECIFIED. ) ;
#1958=CARTESIAN_POINT ( 'NONE',  ( -17.48108435972565644, -24.10675719422536289, -24.29685974197550280 ) ) ;
#1977=CARTESIAN_POINT ( 'NONE',  ( -12.30800288698999978, -24.60220466956999985, -24.01086508779000184 ) ) ;
#1979=CARTESIAN_POINT ( 'NONE',  ( -12.30800288698999978, -24.60220466956999985, -24.01086508779000184 ) ) ;
#2008=CARTESIAN_POINT ( 'NONE',  ( -12.75378086759999796, -32.00000000000000000, -31.28675134614999820 ) ) ;
#2126=CARTESIAN_POINT ( 'NONE',  ( -12.34886039478919173, -23.75151583055949800, -24.50201051798606855 ) ) ;
#2129=B_SPLINE_CURVE_WITH_KNOTS ( 'NONE', 3,
 ( #28979, #14517, #29128, #21599, #664, #26771, #361, #2553, #19229, #24114, #17328, #48, #10099, #14672, #2400, #19389, #19697, #10256, #9942, #12139 ),
 .UNSPECIFIED., .F., .F.,
 ( 4, 1, 1, 1, 2, 2, 2, 1, 1, 1, 2, 2, 4 ),
 ( 0.000000000000000000, 0.1250000000000031641, 0.1875000000000046352, 0.2187500000000062172, 0.2343750000000060785, 0.2500000000000059397, 0.5000000000000045519, 0.6250000000000027756, 0.6875000000000029976, 0.7187500000000029976, 0.7343750000000029976, 0.7500000000000031086, 1.000000000000000000 ),
 .UNSPECIFIED. ) ;
#2139=APPLICATION_CONTEXT ( 'automotive_design' ) ;
#2166=EDGE_CURVE ( 'NONE', #22798, #14380, #26634, .T. ) ;
#2179=CARTESIAN_POINT ( 'NONE',  ( -17.20708009808130612, -31.51741709908550959, -31.56537071389317717 ) ) ;
#2330=CARTESIAN_POINT ( 'NONE',  ( -17.49999999969999820, -32.00000000000000000, -31.28675134614999820 ) ) ;
#2395=FACE_OUTER_BOUND ( 'NONE', #22755, .T. ) ;
#2397=FACE_OUTER_BOUND ( 'NONE', #6665, .T. ) ;
#2400=CARTESIAN_POINT ( 'NONE',  ( -12.39224864153120720, -31.99999999999999289, -27.17394816745003894 ) ) ;
#2519=EDGE_CURVE ( 'NONE', #9043, #24060, #14239, .T. ) ;
#2536=ORIENTED_EDGE ( 'NONE', *, *, #19938, .T. ) ;
#2553=CARTESIAN_POINT ( 'NONE',  ( -12.41253550773259562, -32.00000000000000000, -29.76654229695615683 ) ) ;
#2579=CARTESIAN_POINT ( 'NONE',  ( -12.36045835448409314, -28.65858880358294414, -33.21571233971392445 ) ) ;
#2606=CARTESIAN_POINT ( 'NONE',  ( -17.33922399256787727, -22.00031055996563012, -26.74546041328948576 ) ) ;
#2627=CARTESIAN_POINT ( 'NONE',  ( 0.000000000000000000, 0.000000000000000000, 0.000000000000000000 ) ) ;
#2715=EDGE_CURVE ( 'NONE', #14751, #4997, #24380, .T. ) ;
#2724=CARTESIAN_POINT ( 'NONE',  ( -17.04621913067799710, -32.00000000000000000, -31.28675134614999820 ) ) ;
#2733=CARTESIAN_POINT ( 'NONE',  ( -12.32161713220326327, -29.02784567618598999, -33.00245466908037884 ) ) ;
#2743=CARTESIAN_POINT ( 'NONE',  ( -12.60598845461798767, -26.55662275894602331, -22.88248127776499885 ) ) ;
#2751=VERTEX_POINT ( 'NONE', #10184 ) ;
#2793=CARTESIAN_POINT ( 'NONE',  ( -17.19683899163034724, -26.54814041842956840, -22.88737855935614007 ) ) ;
#2873=CARTESIAN_POINT ( 'NONE',  ( -17.38654519918826935, -31.99979139472987200, -29.76988878280269901 ) ) ;
#2876=VECTOR ( 'NONE', #20015, 1000.000000000000227 ) ;
#2882=CARTESIAN_POINT ( 'NONE',  ( -12.39067510638770209, -28.44925785771653182, -33.33672124906113510 ) ) ;
#2899=AXIS2_PLACEMENT_3D ( 'NONE', #14131, #18842, #4682 ) ;
#2907=EDGE_CURVE ( 'NONE', #24188, #1593, #3843, .T. ) ;
#3016=ORIENTED_EDGE ( 'NONE', *, *, #15574, .T. ) ;
#3118=ORIENTED_EDGE ( 'NONE', *, *, #19072, .T. ) ;
#3171=CARTESIAN_POINT ( 'NONE',  ( -250010.8602219996974, -207625.5434020000102, -380034.9847440001322 ) ) ;
#3261=CARTESIAN_POINT ( 'NONE',  ( -12.59914306489271318, -22.46391341019676702, -31.55459187839498725 ) ) ;
#3290=CARTESIAN_POINT ( 'NONE',  ( -12.30731012794911194, -29.11171768734218546, -23.84543095547712355 ) ) ;
#3306=DIRECTION ( 'NONE',  ( 0.000000000000000000, -0.5000000000001900702, 0.8660254037843290176 ) ) ;
#3394=AXIS2_PLACEMENT_3D ( 'NONE', #25319, #29569, #8151 ) ;
#3401=CARTESIAN_POINT ( 'NONE',  ( -12.29999999980791614, -28.84364015992473895, -30.79900052739454708 ) ) ;
#3403=CIRCLE ( 'NONE', #29530, 4.987531172950001590 ) ;
#3418=AXIS2_PLACEMENT_3D ( 'NONE', #27826, #8003, #17603 ) ;
#3440=CARTESIAN_POINT ( 'NONE',  ( -12.34110296562657894, -28.73347875151786113, -23.62742633845895668 ) ) ;
#3475=CARTESIAN_POINT ( 'NONE',  ( -17.43796590508231503, -30.34944427540625611, -32.23970959347593634 ) ) ;
#3487=CARTESIAN_POINT ( 'NONE',  ( -17.04621913067799710, -27.00000000059169736, -22.62649730796000114 ) ) ;
#3522=EDGE_CURVE ( 'NONE', #1475, #1865, #13243, .T. ) ;
#3594=CARTESIAN_POINT ( 'NONE',  ( -14.89999999913999851, -32.00000000000000000, -25.51324865424999899 ) ) ;
#3604=FACE_OUTER_BOUND ( 'NONE', #7873, .T. ) ;
#3661=ORIENTED_EDGE ( 'NONE', *, *, #12031, .F. ) ;
#3722=CARTESIAN_POINT ( 'NONE',  ( -17.49999999965344344, -27.00000000000000000, -28.40000000020000215 ) ) ;
#3723=CARTESIAN_POINT ( 'NONE',  ( -12.57202792198699370, -22.00000000000000711, -26.18683049397497342 ) ) ;
#3787=B_SPLINE_CURVE_WITH_KNOTS ( 'NONE', 3,
 ( #6551, #25286, #3723, #25763, #23567, #4193, #15847, #22931, #20721, #15675, #13795, #13320, #23410, #1840, #25451, #28262, #11438, #8752, #18360, #29992 ),
 .UNSPECIFIED., .F., .F.,
 ( 4, 1, 1, 1, 2, 2, 2, 1, 1, 1, 2, 2, 4 ),
 ( 0.000000000000000000, 0.1249999999999970302, 0.1874999999999956146, 0.2187499999999950318, 0.2343749999999946432, 0.2499999999999942824, 0.4999999999999947820, 0.6249999999999950040, 0.6874999999999952260, 0.7187499999999952260, 0.7343749999999943379, 0.7499999999999933387, 1.000000000000000000 ),
 .UNSPECIFIED. ) ;
#3799=PRODUCT ( 'Nut M6', 'Nut M6', '', ( #25788 ) ) ;
#3843=LINE ( 'NONE', #25561, #24720 ) ;
#3845=CARTESIAN_POINT ( 'NONE',  ( -17.47798013194186950, -24.05818843344536972, -24.32488866329982358 ) ) ;
#3894=DIRECTION ( 'NONE',  ( -1.000000000000000000, 0.000000000000000000, 0.000000000000000000 ) ) ;
#3926=EDGE_CURVE ( 'NONE', #9909, #1865, #22962, .T. ) ;
#3939=DIRECTION ( 'NONE',  ( 0.000000000000000000, 0.4794255386042043932, 0.8775825618903719816 ) ) ;
#3971=DIRECTION ( 'NONE',  ( 1.000000000000000000, 0.000000000000000000, 0.000000000000000000 ) ) ;
#3980=ORIENTED_EDGE ( 'NONE', *, *, #985, .F. ) ;
#4065=VERTEX_POINT ( 'NONE', #4386 ) ;
#4111=PLANE ( 'NONE',  #11444 ) ;
#4158=CARTESIAN_POINT ( 'NONE',  ( -17.48838570233622747, -24.25553963907254484, -24.21099845983332344 ) ) ;
#4193=CARTESIAN_POINT ( 'NONE',  ( -12.42716818974678894, -22.00000000000000000, -26.94009942549494596 ) ) ;
#4230=CARTESIAN_POINT ( 'NONE',  ( -17.38746449168248276, -28.31653965577788057, -23.38660183296255468 ) ) ;
#4242=CONICAL_SURFACE ( 'NONE', #12279, 4.987531172069999741, 1.047197551199999799 ) ;
#4266=ADVANCED_FACE ( 'NONE', ( #19941 ), #277, .T. ) ;
#4289=EDGE_CURVE ( 'NONE', #29282, #2751, #10032, .T. ) ;
#4305=ORIENTED_EDGE ( 'NONE', *, *, #985, .T. ) ;
#4307=SHAPE_REPRESENTATION_RELATIONSHIP ( 'NONE' , 'NONE' ,  #20626, #26089 ) ;
#4316=CARTESIAN_POINT ( 'NONE',  ( -17.04621913067799710, -22.00000000000000000, -25.51324865357000249 ) ) ;
#4386=CARTESIAN_POINT ( 'NONE',  ( -12.29999999969999891, -30.00000000000000000, -28.40000000020000215 ) ) ;
#4431=ORIENTED_EDGE ( 'NONE', *, *, #4647, .T. ) ;
#4465=DIRECTION ( 'NONE',  ( 1.000000000000000000, 0.000000000000000000, 0.000000000000000000 ) ) ;
#4534=CARTESIAN_POINT ( 'NONE',  ( -17.40441589017246571, -30.57978506141823161, -32.10670460369477297 ) ) ;
#4647=EDGE_CURVE ( 'NONE', #7844, #24648, #28407, .T. ) ;
#4682=DIRECTION ( 'NONE',  ( 0.000000000000000000, 1.000000000000000000, 0.000000000000000000 ) ) ;
#4783=CARTESIAN_POINT ( 'NONE',  ( -17.04621913067799710, -32.00000000058999916, -25.51324865459000080 ) ) ;
#4796=DIRECTION ( 'NONE',  ( 1.000000000000000000, 0.000000000000000000, 0.000000000000000000 ) ) ;
#4830=CARTESIAN_POINT ( 'NONE',  ( -12.30489359501159008, -29.59544839336084010, -32.67501986352419152 ) ) ;
#4906=DIRECTION ( 'NONE',  ( 0.000000000000000000, 1.000000000000000000, 0.000000000000000000 ) ) ;
#4919=CARTESIAN_POINT ( 'NONE',  ( -17.49999999970000175, -29.40181682655888906, -30.23939095857821968 ) ) ;
#4936=CARTESIAN_POINT ( 'NONE',  ( -12.41448843479028241, -28.30844421074986528, -33.41806619590747118 ) ) ;
#4938=CYLINDRICAL_SURFACE ( 'NONE', #9770, 2.999999999999999112 ) ;
#4945=CARTESIAN_POINT ( 'NONE',  ( -12.39150945513257263, -23.44570582929690516, -24.67857000453599881 ) ) ;
#4997=VERTEX_POINT ( 'NONE', #3487 ) ;
#4998=ORIENTED_EDGE ( 'NONE', *, *, #21912, .T. ) ;
#5052=SURFACE_STYLE_USAGE ( .BOTH. , #14360 ) ;
#5079=CARTESIAN_POINT ( 'NONE',  ( -17.42926651579458053, -31.99974916928463031, -27.34261348416758608 ) ) ;
#5163=CARTESIAN_POINT ( 'NONE',  ( -12.29999999974999803, -27.00000000000000000, -28.40000000020000215 ) ) ;
#5198=( LENGTH_UNIT ( ) NAMED_UNIT ( * ) SI_UNIT ( .MILLI., .METRE. ) );
#5206=DIRECTION ( 'NONE',  ( -0.000000000000000000, 1.000000000000000000, 0.000000000000000000 ) ) ;
#5321=CARTESIAN_POINT ( 'NONE',  ( -12.31579099197426075, -24.11373924793705115, -32.50693151577021212 ) ) ;
#5349=CARTESIAN_POINT ( 'NONE',  ( -12.49647831262676512, -27.90203718307900260, -23.14770133019309739 ) ) ;
#5403=CARTESIAN_POINT ( 'NONE',  ( -12.38011772156684920, -25.48083565910511794, -23.50369165914649727 ) ) ;
#5427=CARTESIAN_POINT ( 'NONE',  ( -17.39358994609593267, -22.00021533137563168, -29.72298993498152697 ) ) ;
#5469=CARTESIAN_POINT ( 'NONE',  ( -12.67644879028841309, -26.76800376598850661, -34.03955960393551550 ) ) ;
#5509=DIRECTION ( 'NONE',  ( 0.000000000000000000, 0.000000000000000000, -1.000000000000000000 ) ) ;
#5522=CYLINDRICAL_SURFACE ( 'NONE', #28903, 2.999999999999999112 ) ;
#5544=CARTESIAN_POINT ( 'NONE',  ( -12.38011772158675150, -28.51916434083160112, -33.29630834130933437 ) ) ;
#5624=CARTESIAN_POINT ( 'NONE',  ( -12.75378086759999796, -22.00000000000000000, -25.51324865357000249 ) ) ;
#5679=CARTESIAN_POINT ( 'NONE',  ( -12.29999999969999891, -24.60885018109999933, -24.02302961593000319 ) ) ;
#5898=ADVANCED_FACE ( 'NONE', ( #548 ), #4938, .F. ) ;
#5914=ORIENTED_EDGE ( 'NONE', *, *, #4289, .T. ) ;
#5923=DIRECTION ( 'NONE',  ( 1.000000000000000000, 0.000000000000000000, 0.000000000000000000 ) ) ;
#6075=CARTESIAN_POINT ( 'NONE',  ( -12.29999999991583337, -26.21475634692216161, -31.32191803020494802 ) ) ;
#6198=CARTESIAN_POINT ( 'NONE',  ( -17.49199711315135986, -24.60220466956999985, -24.01086508779000184 ) ) ;
#6355=EDGE_CURVE ( 'NONE', #9043, #29282, #11122, .T. ) ;
#6376=EDGE_LOOP ( 'NONE', ( #30642, #24221, #20913, #22140, #27423, #205, #27783 ) ) ;
#6430=CARTESIAN_POINT ( 'NONE',  ( -17.39611244578981797, -30.63332389908853770, -24.72419783949291627 ) ) ;
#6551=CARTESIAN_POINT ( 'NONE',  ( -12.75378086759999796, -22.00000000000000000, -25.51324865357000249 ) ) ;
#6644=ORIENTED_EDGE ( 'NONE', *, *, #2166, .T. ) ;
#6665=EDGE_LOOP ( 'NONE', ( #19155, #19826, #14563, #18782 ) ) ;
#6712=CARTESIAN_POINT ( 'NONE',  ( -12.31403527400738085, -29.89465053769069414, -32.50227542495312605 ) ) ;
#6797=PLANE ( 'NONE',  #18729 ) ;
#6865=CARTESIAN_POINT ( 'NONE',  ( -12.39529267485836428, -30.57814011873969307, -32.10766253134598003 ) ) ;
#6880=CARTESIAN_POINT ( 'NONE',  ( -17.47798013194552524, -29.94181156654346054, -32.47511133710052889 ) ) ;
#6976=CARTESIAN_POINT ( 'NONE',  ( -17.49999999969999109, -23.99999999999999289, -28.79800326595887583 ) ) ;
#6977=CARTESIAN_POINT ( 'NONE',  ( -14.90000000006999947, -24.00000000000000000, -28.40000000020000215 ) ) ;
#7049=EDGE_LOOP ( 'NONE', ( #15438, #3661 ) ) ;
#7145=CARTESIAN_POINT ( 'NONE',  ( -14.89999999969999855, -27.00000000000000000, -28.40000000020000215 ) ) ;
#7202=ORIENTED_EDGE ( 'NONE', *, *, #20537, .T. ) ;
#7203=CARTESIAN_POINT ( 'NONE',  ( -17.38583936189946755, -25.68983096307264091, -23.38292375445472260 ) ) ;
#7270=DIRECTION ( 'NONE',  ( 1.000000000000000000, 0.000000000000000000, 0.000000000000000000 ) ) ;
#7283=LINE ( 'NONE', #21759, #13453 ) ;
#7304=DIRECTION ( 'NONE',  ( 0.000000000000000000, -1.000000000000000000, 0.000000000000000000 ) ) ;
#7341=CARTESIAN_POINT ( 'NONE',  ( -12.47178235753292697, -31.04315797141627797, -31.83918434892504834 ) ) ;
#7359=CARTESIAN_POINT ( 'NONE',  ( -17.30852986269440308, -26.11984913498134020, -23.13465264714667313 ) ) ;
#7383=ORIENTED_EDGE ( 'NONE', *, *, #6355, .F. ) ;
#7412=FILL_AREA_STYLE ('',( #9933 ) ) ;
#7427=ORIENTED_EDGE ( 'NONE', *, *, #18799, .F. ) ;
#7450=CARTESIAN_POINT ( 'NONE',  ( -12.60598845464734907, -27.44337724096553899, -33.91751872268586965 ) ) ;
#7482=CARTESIAN_POINT ( 'NONE',  ( -17.27724273262455412, -22.00035689406917783, -26.42754666945129927 ) ) ;
#7555=CARTESIAN_POINT ( 'NONE',  ( -12.67644879029220739, -27.23199623400657998, -22.76044039645793049 ) ) ;
#7585=CARTESIAN_POINT ( 'NONE',  ( -17.49999999970000175, -28.83948587665830843, -30.80191174503961449 ) ) ;
#7610=CARTESIAN_POINT ( 'NONE',  ( -12.41634270788144789, -25.70200949929017753, -23.37589838086136496 ) ) ;
#7629=CARTESIAN_POINT ( 'NONE',  ( -17.04621913067799710, -22.00000000000000000, -31.28675134614999820 ) ) ;
#7654=CARTESIAN_POINT ( 'NONE',  ( -17.04621913067799710, -27.00000000059169736, -22.62649730796000114 ) ) ;
#7668=CARTESIAN_POINT ( 'NONE',  ( -12.30731012795045842, -24.88828231266208846, -32.95456904492809258 ) ) ;
#7695=VECTOR ( 'NONE', #11794, 1000.000000000000000 ) ;
#7701=CARTESIAN_POINT ( 'NONE',  ( -12.75378086759999796, -27.00000000059169736, -22.62649730796000114 ) ) ;
#7747=EDGE_CURVE ( 'NONE', #24060, #9909, #30025, .T. ) ;
#7761=CARTESIAN_POINT ( 'NONE',  ( -12.49429647964976375, -26.13498548490847284, -23.12598273097680845 ) ) ;
#7844=VERTEX_POINT ( 'NONE', #29762 ) ;
#7869=FACE_OUTER_BOUND ( 'NONE', #8109, .T. ) ;
#7873=EDGE_LOOP ( 'NONE', ( #28910, #14518, #12384, #30578 ) ) ;
#7910=CARTESIAN_POINT ( 'NONE',  ( -12.39067510636454728, -25.55074214220865514, -23.46327875140281094 ) ) ;
#7917=CIRCLE ( 'NONE', #2899, 2.999999999999999112 ) ;
#8000=ORIENTED_EDGE ( 'NONE', *, *, #21687, .T. ) ;
#8003=DIRECTION ( 'NONE',  ( -1.000000000000000000, 0.000000000000000000, 0.000000000000000000 ) ) ;
#8017=EDGE_CURVE ( 'NONE', #24648, #7844, #17925, .T. ) ;
#8109=EDGE_LOOP ( 'NONE', ( #15872, #29321, #20673, #25855 ) ) ;
#8110=ORIENTED_EDGE ( 'NONE', *, *, #6355, .T. ) ;
#8120=LINE ( 'NONE', #24822, #24573 ) ;
#8124=CARTESIAN_POINT ( 'NONE',  ( -12.48413792322910965, -22.90323034870550600, -31.80782553739934571 ) ) ;
#8125=CARTESIAN_POINT ( 'NONE',  ( -12.30000000006999805, -24.00000000000000000, -28.40000000020000215 ) ) ;
#8151=DIRECTION ( 'NONE',  ( 0.000000000000000000, 1.000000000000000000, 0.000000000000000000 ) ) ;
#8272=CARTESIAN_POINT ( 'NONE',  ( -12.30000000005458460, -24.00000000000000711, -28.79269908189872851 ) ) ;
#8275=CARTESIAN_POINT ( 'NONE',  ( -17.45872973692355501, -25.26842553675004410, -33.17377770962026062 ) ) ;
#8301=VERTEX_POINT ( 'NONE', #10350 ) ;
#8384=AXIS2_PLACEMENT_3D ( 'NONE', #18392, #11006, #11474 ) ;
#8423=CARTESIAN_POINT ( 'NONE',  ( -12.29999999999291660, -24.60099947280545152, -30.24364016012474110 ) ) ;
#8473=EDGE_CURVE ( 'NONE', #14200, #16868, #3787, .T. ) ;
#8480=CARTESIAN_POINT ( 'NONE',  ( -17.48914026050856663, -29.21618945753110097, -32.89398511221816079 ) ) ;
#8553=PRODUCT_DEFINITION_SHAPE ( 'NONE', 'NONE',  #18101 ) ;
#8707=CARTESIAN_POINT ( 'NONE',  ( -17.40850972537708330, -23.44589038181687712, -24.67846847529753518 ) ) ;
#8712=CARTESIAN_POINT ( 'NONE',  ( -17.49999999969999820, -27.00000000000000000, -28.40000000020000215 ) ) ;
#8713=EDGE_CURVE ( 'NONE', #22798, #11502, #7917, .T. ) ;
#8751=CARTESIAN_POINT ( 'NONE',  ( -17.39611244578438232, -23.36667610088668212, -32.07580216089276348 ) ) ;
#8752=CARTESIAN_POINT ( 'NONE',  ( -12.48017473518528320, -22.00000000000000000, -30.22182049597928000 ) ) ;
#8781=AXIS2_PLACEMENT_3D ( 'NONE', #8712, #18318, #23679 ) ;
#8940=CARTESIAN_POINT ( 'NONE',  ( -17.49285076559436902, -29.59593888003697870, -32.67472628167575266 ) ) ;
#8944=CARTESIAN_POINT ( 'NONE',  ( -17.39988487663317329, -30.61060157591113651, -24.71107910008982245 ) ) ;
#9043=VERTEX_POINT ( 'NONE', #30933 ) ;
#9086=ORIENTED_EDGE ( 'NONE', *, *, #20348, .F. ) ;
#9095=( GEOMETRIC_REPRESENTATION_CONTEXT ( 3 ) GLOBAL_UNCERTAINTY_ASSIGNED_CONTEXT ( ( #872 ) ) GLOBAL_UNIT_ASSIGNED_CONTEXT ( ( #5198, #23958, #21904 ) ) REPRESENTATION_CONTEXT ( 'NONE', 'WORKASPACE' ) );
#9211=CARTESIAN_POINT ( 'NONE',  ( -17.39988487662844108, -23.38939842406737313, -32.08892090029773669 ) ) ;
#9223=CARTESIAN_POINT ( 'NONE',  ( -12.34886039477888175, -30.24848416943050822, -32.29798948241971601 ) ) ;
#9226=DIRECTION ( 'NONE',  ( 1.000000000000000000, 0.000000000000000000, 0.000000000000000000 ) ) ;
#9252=COLOUR_RGB ( '', 0.09019608, 0.27058824, 0.51372549) ;
#9267=LINE ( 'NONE', #20929, #7695 ) ;
#9293=DIRECTION ( 'NONE',  ( -0.000000000000000000, 0.5000000000001900702, 0.8660254037843290176 ) ) ;
#9321=EDGE_LOOP ( 'NONE', ( #5914, #7202, #7427, #9940 ) ) ;
#9325=CARTESIAN_POINT ( 'NONE',  ( -17.49999999969999820, -29.61919234679800894, -29.91462304360321411 ) ) ;
#9367=CARTESIAN_POINT ( 'NONE',  ( -17.04621913067799710, -22.00000000000000000, -31.28675134614999820 ) ) ;
#9392=DIRECTION ( 'NONE',  ( 0.000000000000000000, -0.8660254037843289066, 0.5000000000001899592 ) ) ;
#9399=CARTESIAN_POINT ( 'NONE',  ( -17.45644675878136098, -30.19649537162369057, -32.32803605695916360 ) ) ;
#9513=EDGE_CURVE ( 'NONE', #1593, #11462, #3403, .T. ) ;
#9516=CARTESIAN_POINT ( 'NONE',  ( 249981.0602220003202, -207625.5434020000102, -380034.9847440001322 ) ) ;
#9548=EDGE_CURVE ( 'NONE', #11502, #22798, #16815, .T. ) ;
#9645=CARTESIAN_POINT ( 'NONE',  ( -17.27724273263302379, -31.99964310593069072, -30.37245333090922728 ) ) ;
#9649=EDGE_CURVE ( 'NONE', #26486, #14200, #7283, .T. ) ;
#9770=AXIS2_PLACEMENT_3D ( 'NONE', #7145, #4796, #7304 ) ;
#9825=CARTESIAN_POINT ( 'NONE',  ( -12.30489359501477864, -24.40455160664326684, -24.12498013687346443 ) ) ;
#9909=VERTEX_POINT ( 'NONE', #11962 ) ;
#9923=CARTESIAN_POINT ( 'NONE',  ( -12.40047914203026380, -30.61031961594332529, -24.71115946178905176 ) ) ;
#9933=FILL_AREA_STYLE_COLOUR ( '', #590 ) ;
#9940=ORIENTED_EDGE ( 'NONE', *, *, #13004, .F. ) ;
#9942=CARTESIAN_POINT ( 'NONE',  ( -12.59531001298080710, -31.99999999999998579, -26.06220780008972326 ) ) ;
#10032=B_SPLINE_CURVE_WITH_KNOTS ( 'NONE', 3,
 ( #27176, #22618, #1059, #10502, #29690, #24969, #20241, #18189, #8275, #17869, #15520, #25126, #13156, #20404, #30786, #9211, #8751, #18972, #28261, #9367 ),
 .UNSPECIFIED., .F., .F.,
 ( 4, 1, 1, 1, 2, 2, 2, 1, 1, 1, 2, 2, 4 ),
 ( 0.000000000000000000, 0.1250000000000018596, 0.1875000000000018874, 0.2187500000000019151, 0.2343750000000011935, 0.2500000000000004441, 0.4999999999999968914, 0.6249999999999951150, 0.6874999999999942268, 0.7187499999999937828, 0.7343749999999943379, 0.7499999999999948930, 1.000000000000000000 ),
 .UNSPECIFIED. ) ;
#10049=CARTESIAN_POINT ( 'NONE',  ( -12.44385388530932701, -25.85073127557643247, -33.50965282259626576 ) ) ;
#10099=CARTESIAN_POINT ( 'NONE',  ( -12.35698168758728777, -32.00000000000000711, -27.45509309272506826 ) ) ;
#10184=CARTESIAN_POINT ( 'NONE',  ( -17.04621913067799710, -22.00000000000000000, -31.28675134614999820 ) ) ;
#10202=CARTESIAN_POINT ( 'NONE',  ( -12.38103409318511083, -23.51166759135386641, -32.15925398282187331 ) ) ;
#10256=CARTESIAN_POINT ( 'NONE',  ( -12.48017473518110521, -32.00000000000000000, -26.57817950442041166 ) ) ;
#10350=CARTESIAN_POINT ( 'NONE',  ( -12.75378086759999796, -27.00000000000000355, -34.17350269210000135 ) ) ;
#10358=CARTESIAN_POINT ( 'NONE',  ( -12.39443769393808559, -23.42635292539874214, -32.11001460377168115 ) ) ;
#10385=CARTESIAN_POINT ( 'NONE',  ( -12.60902638016457544, -27.45788211093552889, -22.89113855904373906 ) ) ;
#10451=SURFACE_SIDE_STYLE ('',( #15325 ) ) ;
#10454=VECTOR ( 'NONE', #21577, 1000.000000000000000 ) ;
#10500=CARTESIAN_POINT ( 'NONE',  ( -12.29999999969999891, -30.00000000000000000, -28.40000000020000215 ) ) ;
#10502=CARTESIAN_POINT ( 'NONE',  ( -17.31926949172594377, -26.03170168038248633, -33.61445539661270487 ) ) ;
#10594=CARTESIAN_POINT ( 'NONE',  ( -12.75378086759999796, -27.00000000059169736, -22.62649730796000114 ) ) ;
#10636=EDGE_CURVE ( 'NONE', #17371, #11462, #29759, .T. ) ;
#10681=FACE_BOUND ( 'NONE', #7049, .T. ) ;
#10715=ORIENTED_EDGE ( 'NONE', *, *, #12031, .T. ) ;
#10717=CARTESIAN_POINT ( 'NONE',  ( -17.41454186825435357, -30.51562454719971385, -32.14375470241721899 ) ) ;
#10735=ADVANCED_FACE ( 'NONE', ( #14029 ), #4111, .T. ) ;
#10848=CARTESIAN_POINT ( 'NONE',  ( -17.38249745079332698, -28.28848602987763527, -23.37040506449729094 ) ) ;
#10871=ORIENTED_EDGE ( 'NONE', *, *, #2166, .F. ) ;
#10942=EDGE_CURVE ( 'NONE', #4997, #9909, #27617, .T. ) ;
#10966=DIRECTION ( 'NONE',  ( 0.000000000000000000, -0.4794255386042043932, -0.8775825618903719816 ) ) ;
#10978=PLANE ( 'NONE',  #23586 ) ;
#11006=DIRECTION ( 'NONE',  ( -1.000000000000000000, 0.000000000000000000, 0.000000000000000000 ) ) ;
#11021=FACE_OUTER_BOUND ( 'NONE', #14836, .T. ) ;
#11067=CARTESIAN_POINT ( 'NONE',  ( -17.49999999969999820, -24.00000000000000000, -28.40000000020000215 ) ) ;
#11086=CARTESIAN_POINT ( 'NONE',  ( -17.20708009806455507, -22.48258290086466360, -25.23462928653505344 ) ) ;
#11122=B_SPLINE_CURVE_WITH_KNOTS ( 'NONE', 3,
 ( #30047, #8480, #1886, #30530, #28160, #18077, #11485, #20607, #27681, #30205, #15722 ),
 .UNSPECIFIED., .F., .F.,
 ( 4, 1, 1, 1, 2, 2, 4 ),
 ( 0.000000000000000000, 0.2500000000000012768, 0.3750000000000018874, 0.4375000000000022204, 0.4687500000000023870, 0.5000000000000025535, 1.000000000000000000 ),
 .UNSPECIFIED. ) ;
#11152=EDGE_LOOP ( 'NONE', ( #14461, #7383, #17475, #13258, #23927, #4305, #26630 ) ) ;
#11184=VERTEX_POINT ( 'NONE', #15371 ) ;
#11227=DIRECTION ( 'NONE',  ( -1.000000000000000000, 0.000000000000000000, 0.000000000000000000 ) ) ;
#11236=CARTESIAN_POINT ( 'NONE',  ( -17.45644675878112650, -23.80350462838311998, -24.47196394343449199 ) ) ;
#11368=FACE_BOUND ( 'NONE', #18095, .T. ) ;
#11438=CARTESIAN_POINT ( 'NONE',  ( -12.40388755361936468, -22.00000000000000000, -29.70864971667464971 ) ) ;
#11444=AXIS2_PLACEMENT_3D ( 'NONE', #16378, #9293, #30704 ) ;
#11462=VERTEX_POINT ( 'NONE', #11647 ) ;
#11466=CARTESIAN_POINT ( 'NONE',  ( -17.40256142132136929, -30.59124499734533131, -32.10008654271492645 ) ) ;
#11474=DIRECTION ( 'NONE',  ( 0.000000000000000000, 1.000000000000000000, 0.000000000000000000 ) ) ;
#11485=CARTESIAN_POINT ( 'NONE',  ( -17.38968115012163196, -28.33218551802936602, -33.40436502465443169 ) ) ;
#11502=VERTEX_POINT ( 'NONE', #18295 ) ;
#11571=LINE ( 'NONE', #9516, #22669 ) ;
#11616=CARTESIAN_POINT ( 'NONE',  ( -17.49199711315135986, -29.39779533043000015, -32.78913491261000246 ) ) ;
#11647=CARTESIAN_POINT ( 'NONE',  ( -12.29999999969999891, -29.39114981890000067, -32.77697038446999755 ) ) ;
#11666=ADVANCED_FACE ( 'NONE', ( #10681, #25479 ), #18218, .T. ) ;
#11697=EDGE_CURVE ( 'NONE', #11462, #1593, #11968, .T. ) ;
#11747=CARTESIAN_POINT ( 'NONE',  ( -12.39150945512032109, -30.55429417067527709, -32.12142999588005665 ) ) ;
#11770=ORIENTED_EDGE ( 'NONE', *, *, #10636, .T. ) ;
#11794=DIRECTION ( 'NONE',  ( 1.000000000000000000, 0.000000000000000000, 0.000000000000000000 ) ) ;
#11882=EDGE_LOOP ( 'NONE', ( #2536, #10715, #10871, #13134 ) ) ;
#11962=CARTESIAN_POINT ( 'NONE',  ( -17.04621913067799710, -32.00000000058999916, -25.51324865459000080 ) ) ;
#11968=CIRCLE ( 'NONE', #3418, 4.987531172950001590 ) ;
#11992=B_SPLINE_CURVE_WITH_KNOTS ( 'NONE', 3,
 ( #17046, #21776, #2733, #386, #2579, #5544, #2882, #26957, #26494, #4936, #19570, #22088, #7450, #17505 ),
 .UNSPECIFIED., .F., .F.,
 ( 4, 2, 2, 1, 1, 2, 2, 4 ),
 ( 0.000000000000000000, 0.2500000000000167644, 0.3750000000000232592, 0.4375000000000246470, 0.4687500000000254796, 0.4843750000000243694, 0.5000000000000232037, 1.000000000000000000 ),
 .UNSPECIFIED. ) ;
#12031=EDGE_CURVE ( 'NONE', #4065, #14380, #1328, .T. ) ;
#12110=VECTOR ( 'NONE', #28496, 1000.000000000000000 ) ;
#12139=CARTESIAN_POINT ( 'NONE',  ( -12.75378086759999796, -32.00000000058999916, -25.51324865459000080 ) ) ;
#12161=LINE ( 'NONE', #29885, #17008 ) ;
#12200=CARTESIAN_POINT ( 'NONE',  ( -17.48420900742436146, -22.00016259987420852, -28.84610937565356892 ) ) ;
#12279=AXIS2_PLACEMENT_3D ( 'NONE', #25966, #18406, #3939 ) ;
#12314=CARTESIAN_POINT ( 'NONE',  ( -17.49999999969999465, -26.60251055750184079, -31.40006728715443529 ) ) ;
#12320=CARTESIAN_POINT ( 'NONE',  ( -17.38918303935544074, -31.99979622920404054, -29.75246175266256898 ) ) ;
#12359=CARTESIAN_POINT ( 'NONE',  ( -17.39952085737127518, -22.00021057524676849, -29.68220823416547205 ) ) ;
#12384=ORIENTED_EDGE ( 'NONE', *, *, #25559, .T. ) ;
#12458=CARTESIAN_POINT ( 'NONE',  ( -17.49999999969999465, -24.07621958799680328, -29.18059818862752053 ) ) ;
#12465=CARTESIAN_POINT ( 'NONE',  ( -17.44828348017973596, -31.99970846322542428, -27.51010410072800738 ) ) ;
#12485=CARTESIAN_POINT ( 'NONE',  ( -12.31092893605833538, -24.78820930377925791, -23.90347526215919416 ) ) ;
#12553=CARTESIAN_POINT ( 'NONE',  ( -12.40457278470412206, -23.36520658321533617, -32.07470739609649968 ) ) ;
#12619=CARTESIAN_POINT ( 'NONE',  ( -17.39542721470322917, -31.99978666472101096, -27.08953026176062195 ) ) ;
#12703=CARTESIAN_POINT ( 'NONE',  ( -12.49647831262057451, -26.09796281691805575, -33.65229867019547072 ) ) ;
#12710=DIRECTION ( 'NONE',  ( 0.000000000000000000, -0.4794255386042043932, -0.8775825618903719816 ) ) ;
#12728=ORIENTED_EDGE ( 'NONE', *, *, #8713, .T. ) ;
#12895=CARTESIAN_POINT ( 'NONE',  ( -12.31579099197323934, -29.88626075205729293, -24.29306848462797319 ) ) ;
#12900=ORIENTED_EDGE ( 'NONE', *, *, #16530, .F. ) ;
#12960=PRESENTATION_STYLE_ASSIGNMENT (( #17367 ) ) ;
#13004=EDGE_CURVE ( 'NONE', #29282, #8301, #8120, .T. ) ;
#13005=CARTESIAN_POINT ( 'NONE',  ( -12.29999999996208437, -25.15635984007525749, -30.79900052739454708 ) ) ;
#13043=CARTESIAN_POINT ( 'NONE',  ( -12.41345480022817860, -28.31353721119876354, -23.38510924739736652 ) ) ;
#13058=CARTESIAN_POINT ( 'NONE',  ( -17.49999999969999820, -27.00000000000002487, -22.62649730830000294 ) ) ;
#13073=CARTESIAN_POINT ( 'NONE',  ( -17.32507820271158039, -31.06130891780428271, -31.82860708177667064 ) ) ;
#13134=ORIENTED_EDGE ( 'NONE', *, *, #9548, .F. ) ;
#13145=ORIENTED_EDGE ( 'NONE', *, *, #4647, .F. ) ;
#13156=CARTESIAN_POINT ( 'NONE',  ( -17.44301831181765650, -23.68168661394991759, -32.25767356540747244 ) ) ;
#13200=PLANE ( 'NONE',  #25365 ) ;
#13221=ORIENTED_EDGE ( 'NONE', *, *, #3522, .T. ) ;
#13243=B_SPLINE_CURVE_WITH_KNOTS ( 'NONE', 3,
 ( #7701, #7555, #10385, #29572, #5349, #22344, #15253, #29258, #796, #13043, #25006, #3440, #3290, #17145, #12895, #17455, #24400, #14954, #340, #646, #9923, #15106, #14801, #24552, #19523, #22045 ),
 .UNSPECIFIED., .F., .F.,
 ( 4, 2, 2, 1, 1, 2, 2, 2, 2, 2, 1, 1, 2, 2, 4 ),
 ( 0.000000000000000000, 0.1249999999999981959, 0.1874999999999982792, 0.2187499999999980016, 0.2343749999999985012, 0.2421874999999975575, 0.2499999999999966138, 0.4999999999999827915, 0.6249999999999750200, 0.6874999999999706901, 0.7187499999999685807, 0.7343749999999680256, 0.7421874999999686917, 0.7499999999999693578, 1.000000000000000000 ),
 .UNSPECIFIED. ) ;
#13258=ORIENTED_EDGE ( 'NONE', *, *, #8017, .F. ) ;
#13265=( NAMED_UNIT ( * ) SI_UNIT ( $, .STERADIAN. ) SOLID_ANGLE_UNIT ( ) );
#13270=EDGE_CURVE ( 'NONE', #26486, #2751, #24502, .T. ) ;
#13277=CARTESIAN_POINT ( 'NONE',  ( -17.48633009204635869, -24.20600253127152612, -24.23958570799475254 ) ) ;
#13283=AXIS2_PLACEMENT_3D ( 'NONE', #21743, #5206, #7270 ) ;
#13319=DIRECTION ( 'NONE',  ( 1.000000000000000000, 0.000000000000000000, 0.000000000000000000 ) ) ;
#13320=CARTESIAN_POINT ( 'NONE',  ( -12.32027642597305039, -21.99999999999999645, -28.95335161925533640 ) ) ;
#13453=VECTOR ( 'NONE', #16871, 1000.000000000000000 ) ;
#13510=CARTESIAN_POINT ( 'NONE',  ( -17.49230054464772977, -29.69120553467622869, -24.18026554819070739 ) ) ;
#13670=CARTESIAN_POINT ( 'NONE',  ( -17.45872973692405594, -28.73157446327232734, -23.62622229079265779 ) ) ;
#13795=CARTESIAN_POINT ( 'NONE',  ( -12.30769945475813643, -22.00000000000000000, -28.62078513402536473 ) ) ;
#13830=CARTESIAN_POINT ( 'NONE',  ( -17.44301831181996221, -30.31831338603490167, -24.54232643498374244 ) ) ;
#14015=DIRECTION ( 'NONE',  ( 0.000000000000000000, 0.000000000000000000, 1.000000000000000000 ) ) ;
#14029=FACE_OUTER_BOUND ( 'NONE', #22082, .T. ) ;
#14042=DIRECTION ( 'NONE',  ( 0.000000000000000000, 1.000000000000000000, 0.000000000000000000 ) ) ;
#14131=CARTESIAN_POINT ( 'NONE',  ( -17.49999999932747130, -27.00000000000000000, -28.40000000020000215 ) ) ;
#14162=ORIENTED_EDGE ( 'NONE', *, *, #21912, .F. ) ;
#14200=VERTEX_POINT ( 'NONE', #5624 ) ;
#14239=B_SPLINE_CURVE_WITH_KNOTS ( 'NONE', 3,
 ( #11616, #21213, #8940, #18848, #28448, #23271, #6880, #16637, #9399, #3475, #16485, #10717, #26098, #4534, #11466, #13073, #2179, #20316 ),
 .UNSPECIFIED., .F., .F.,
 ( 4, 2, 2, 2, 2, 1, 1, 2, 2, 4 ),
 ( 0.000000000000000000, 0.1249999999999931166, 0.1874999999999897304, 0.2499999999999863443, 0.3749999999999832356, 0.4374999999999815148, 0.4687499999999824585, 0.4843749999999824030, 0.4999999999999824585, 1.000000000000000000 ),
 .UNSPECIFIED. ) ;
#14240=CARTESIAN_POINT ( 'NONE',  ( -12.75378086759999796, -22.00000000000000000, -25.51324865357000249 ) ) ;
#14274=CARTESIAN_POINT ( 'NONE',  ( -12.38365826779466161, -30.50317931097972846, -32.15094117388489536 ) ) ;
#14308=ORIENTED_EDGE ( 'NONE', *, *, #2715, .T. ) ;
#14315=ADVANCED_FACE ( 'NONE', ( #1382 ), #10978, .T. ) ;
#14344=LINE ( 'NONE', #23943, #10454 ) ;
#14360=SURFACE_SIDE_STYLE ('',( #26763 ) ) ;
#14368=ORIENTED_EDGE ( 'NONE', *, *, #9513, .F. ) ;
#14376=CARTESIAN_POINT ( 'NONE',  ( -17.49999999969999820, -27.39748944249814855, -31.39993271324557256 ) ) ;
#14380=VERTEX_POINT ( 'NONE', #8125 ) ;
#14418=UNCERTAINTY_MEASURE_WITH_UNIT (LENGTH_MEASURE( 1.000000000000000082E-05 ), #17974, 'distance_accuracy_value', 'NONE');
#14420=CARTESIAN_POINT ( 'NONE',  ( -17.38918303935042431, -22.00020377080068812, -27.04753824768668835 ) ) ;
#14461=ORIENTED_EDGE ( 'NONE', *, *, #4289, .F. ) ;
#14517=CARTESIAN_POINT ( 'NONE',  ( -12.67459614424497794, -32.00000000000000711, -31.01244741568594776 ) ) ;
#14518=ORIENTED_EDGE ( 'NONE', *, *, #15191, .T. ) ;
#14535=CARTESIAN_POINT ( 'NONE',  ( -17.40556230546876648, -31.99979043241261323, -27.16013815127665154 ) ) ;
#14556=CARTESIAN_POINT ( 'NONE',  ( -12.47178235754251219, -22.95684202855160194, -24.96081565149350823 ) ) ;
#14563=ORIENTED_EDGE ( 'NONE', *, *, #8473, .T. ) ;
#14672=CARTESIAN_POINT ( 'NONE',  ( -12.38084235052808246, -32.00000000000000000, -27.25842518461809760 ) ) ;
#14751=VERTEX_POINT ( 'NONE', #18328 ) ;
#14801=CARTESIAN_POINT ( 'NONE',  ( -12.40641005330639501, -30.64563522679841867, -24.73155443112704432 ) ) ;
#14836=EDGE_LOOP ( 'NONE', ( #26404, #525, #3016, #13145, #9086, #29208, #26016 ) ) ;
#14886=CARTESIAN_POINT ( 'NONE',  ( -17.30352168678310676, -22.00035733197351107, -26.55503778092711187 ) ) ;
#14925=CARTESIAN_POINT ( 'NONE',  ( -12.34115088265052940, -23.82565491187611428, -32.34044972036594601 ) ) ;
#14954=CARTESIAN_POINT ( 'NONE',  ( -12.37073348361184699, -30.41559816918431025, -24.59878346509346159 ) ) ;
#14995=CARTESIAN_POINT ( 'NONE',  ( -17.45884911675408091, -31.99970210406505444, -27.62116137362975721 ) ) ;
#15038=CARTESIAN_POINT ( 'NONE',  ( -17.37426278432861082, -22.00023419291344240, -26.95111891605012744 ) ) ;
#15082=FACE_OUTER_BOUND ( 'NONE', #30774, .T. ) ;
#15106=CARTESIAN_POINT ( 'NONE',  ( -12.40457278470585756, -30.63479341678588952, -24.72529260430050257 ) ) ;
#15126=DIRECTION ( 'NONE',  ( 0.000000000000000000, 1.000000000000000000, 0.000000000000000000 ) ) ;
#15157=CARTESIAN_POINT ( 'NONE',  ( -12.41036288878599336, -25.66802163662577385, -23.39552330665722479 ) ) ;
#15191=EDGE_CURVE ( 'NONE', #24060, #11184, #14344, .T. ) ;
#15223=CARTESIAN_POINT ( 'NONE',  ( -12.46077600683748265, -25.93302859383775427, -33.55712785976603385 ) ) ;
#15253=CARTESIAN_POINT ( 'NONE',  ( -12.44385388531385495, -28.14926872442419281, -23.29034717779581598 ) ) ;
#15325=SURFACE_STYLE_FILL_AREA ( #20046 ) ;
#15370=CARTESIAN_POINT ( 'NONE',  ( -12.29999999986958414, -27.39269908169872281, -31.40000000020000570 ) ) ;
#15371=CARTESIAN_POINT ( 'NONE',  ( -12.75378086759999796, -32.00000000000000000, -31.28675134614999820 ) ) ;
#15438=ORIENTED_EDGE ( 'NONE', *, *, #20701, .F. ) ;
#15520=CARTESIAN_POINT ( 'NONE',  ( -17.49230054464816320, -24.30879446532417276, -32.61973445220952073 ) ) ;
#15553=DIRECTION ( 'NONE',  ( 1.000000000000000000, 0.000000000000000000, 0.000000000000000000 ) ) ;
#15574=EDGE_CURVE ( 'NONE', #14751, #24648, #12161, .T. ) ;
#15635=CARTESIAN_POINT ( 'NONE',  ( -17.41454186824532258, -23.48437545276489047, -24.65624529799447018 ) ) ;
#15675=CARTESIAN_POINT ( 'NONE',  ( -12.30772508779121921, -22.00000000000000711, -27.95972194141362976 ) ) ;
#15700=SHAPE_DEFINITION_REPRESENTATION ( #8553, #20626 ) ;
#15722=CARTESIAN_POINT ( 'NONE',  ( -17.04621913067799710, -27.00000000000000355, -34.17350269210000135 ) ) ;
#15847=CARTESIAN_POINT ( 'NONE',  ( -12.41750254861463354, -21.99999999999999289, -27.00106416659522779 ) ) ;
#15872=ORIENTED_EDGE ( 'NONE', *, *, #10942, .T. ) ;
#15905=ORIENTED_EDGE ( 'NONE', *, *, #15191, .F. ) ;
#16027=CARTESIAN_POINT ( 'NONE',  ( -17.22797207741495029, -27.58333898473983581, -22.96328822816851201 ) ) ;
#16089=DIRECTION ( 'NONE',  ( -1.000000000000000000, 0.000000000000000000, 0.000000000000000000 ) ) ;
#16097=ORIENTED_EDGE ( 'NONE', *, *, #11697, .T. ) ;
#16378=CARTESIAN_POINT ( 'NONE',  ( -17.49999999969999820, -22.00000000000000000, -25.51324865424999899 ) ) ;
#16395=DIRECTION ( 'NONE',  ( 1.000000000000000000, 0.000000000000000000, 0.000000000000000000 ) ) ;
#16458=VECTOR ( 'NONE', #15553, 1000.000000000000000 ) ;
#16485=CARTESIAN_POINT ( 'NONE',  ( -17.42785659857645086, -30.42600657595649949, -32.19550051884773012 ) ) ;
#16530=EDGE_CURVE ( 'NONE', #17371, #8301, #11992, .T. ) ;
#16564=CARTESIAN_POINT ( 'NONE',  ( -17.49999999969999820, -24.38109793998400932, -29.91497134778435907 ) ) ;
#16637=CARTESIAN_POINT ( 'NONE',  ( -17.46645031549716620, -30.09476775824673211, -32.38680219110657532 ) ) ;
#16684=CARTESIAN_POINT ( 'NONE',  ( -14.89999999913999851, -22.00000000000000000, -31.28675134614999820 ) ) ;
#16710=CARTESIAN_POINT ( 'NONE',  ( -17.49999999970000175, -25.16060904162269907, -30.80181682675910437 ) ) ;
#16717=CARTESIAN_POINT ( 'NONE',  ( -17.49268987145706689, -32.00023133968888089, -28.84848335963180332 ) ) ;
#16815=B_SPLINE_CURVE_WITH_KNOTS ( 'NONE', 3,
 ( #26783, #26477, #28680, #9325, #4919, #7585, #17180, #18927, #14376, #12314, #26326, #31047, #16710, #28525, #16564, #12458, #6976, #19398 ),
 .UNSPECIFIED., .F., .F.,
 ( 4, 2, 2, 2, 2, 2, 2, 2, 4 ),
 ( 0.000000000000000000, 0.1250000000000001665, 0.2500000000000003331, 0.3750000000000004996, 0.5000000000000006661, 0.6250000000000008882, 0.7500000000000005551, 0.8750000000000002220, 1.000000000000000000 ),
 .UNSPECIFIED. ) ;
#16816=DIRECTION ( 'NONE',  ( -1.000000000000000000, 0.000000000000000000, 0.000000000000000000 ) ) ;
#16859=CARTESIAN_POINT ( 'NONE',  ( -17.49999999969999820, -24.60885018109999933, -24.02302961593000319 ) ) ;
#16868=VERTEX_POINT ( 'NONE', #24246 ) ;
#16871=DIRECTION ( 'NONE',  ( 1.000000000000000000, 0.000000000000000000, 0.000000000000000000 ) ) ;
#16918=UNCERTAINTY_MEASURE_WITH_UNIT (LENGTH_MEASURE( 1.000000000000000082E-05 ), #29643, 'distance_accuracy_value', 'NONE');
#16920=CARTESIAN_POINT ( 'NONE',  ( -17.35614611409699393, -22.00027648907067501, -26.84046950015551047 ) ) ;
#17008=VECTOR ( 'NONE', #22350, 1000.000000000000227 ) ;
#17038=CARTESIAN_POINT ( 'NONE',  ( -17.39358994610300257, -31.99978466862134141, -27.07701006545490330 ) ) ;
#17046=CARTESIAN_POINT ( 'NONE',  ( -12.30800288698999978, -29.39779533043000015, -32.78913491261000246 ) ) ;
#17056=CARTESIAN_POINT ( 'NONE',  ( -12.39529267487105102, -23.42185988122897555, -24.69233746907211469 ) ) ;
#17076=CARTESIAN_POINT ( 'NONE',  ( -17.31586207617448636, -22.00035168746386560, -30.24399382304843797 ) ) ;
#17145=CARTESIAN_POINT ( 'NONE',  ( -12.30733375691920628, -29.69486568737967502, -24.18213133546005977 ) ) ;
#17180=CARTESIAN_POINT ( 'NONE',  ( -17.49999999970000175, -28.51480899498708510, -31.01896946163343216 ) ) ;
#17298=MECHANICAL_DESIGN_GEOMETRIC_PRESENTATION_REPRESENTATION('',(#17802),#26874);
#17328=CARTESIAN_POINT ( 'NONE',  ( -12.30769945475714344, -32.00000000000001421, -28.17921486638179829 ) ) ;
#17336=ORIENTED_EDGE ( 'NONE', *, *, #8713, .F. ) ;
#17347=CARTESIAN_POINT ( 'NONE',  ( -17.49266624248391722, -32.00021425718040291, -28.17511218750900071 ) ) ;
#17367=SURFACE_STYLE_USAGE ( .BOTH. , #10451 ) ;
#17371=VERTEX_POINT ( 'NONE', #23839 ) ;
#17426=CARTESIAN_POINT ( 'NONE',  ( -12.75378086759999796, -22.00000000000000000, -31.28675134614999820 ) ) ;
#17455=CARTESIAN_POINT ( 'NONE',  ( -12.34115088265029669, -30.17434508811917127, -24.45955028003077913 ) ) ;
#17475=ORIENTED_EDGE ( 'NONE', *, *, #20348, .T. ) ;
#17505=CARTESIAN_POINT ( 'NONE',  ( -12.75378086759999796, -27.00000000000000355, -34.17350269210000135 ) ) ;
#17577=CARTESIAN_POINT ( 'NONE',  ( -12.30733375692050302, -24.30513431261573842, -32.61786866493986992 ) ) ;
#17603=DIRECTION ( 'NONE',  ( 0.000000000000000000, 1.000000000000000000, 0.000000000000000000 ) ) ;
#17702=ADVANCED_FACE ( 'NONE', ( #11368, #2395 ), #6797, .F. ) ;
#17710=CARTESIAN_POINT ( 'NONE',  ( -12.29999999971541591, -30.00000000000000000, -28.79269908189872851 ) ) ;
#17722=AXIS2_PLACEMENT_3D ( 'NONE', #2627, #14015, #29203 ) ;
#17724=CONICAL_SURFACE ( 'NONE', #25298, 4.987531172069999741, 1.047197551199999799 ) ;
#17802=STYLED_ITEM ( 'NONE', ( #12960 ), #26089 ) ;
#17869=CARTESIAN_POINT ( 'NONE',  ( -17.49227491161553871, -24.88129198361984606, -32.95026604850808383 ) ) ;
#17925=CIRCLE ( 'NONE', #8384, 4.987531172950001590 ) ;
#17974=( LENGTH_UNIT ( ) NAMED_UNIT ( * ) SI_UNIT ( .MILLI., .METRE. ) );
#18061=CARTESIAN_POINT ( 'NONE',  ( -17.12540385515261931, -27.23755417213825325, -22.76364927353119683 ) ) ;
#18077=CARTESIAN_POINT ( 'NONE',  ( -17.39770507059490967, -28.37940622391889178, -33.37710213739777032 ) ) ;
#18095=EDGE_LOOP ( 'NONE', ( #814, #12728 ) ) ;
#18101=PRODUCT_DEFINITION ( 'UNKNOWN', '', #22907, #19441 ) ;
#18113=EDGE_CURVE ( 'NONE', #4997, #1475, #9267, .T. ) ;
#18187=CARTESIAN_POINT ( 'NONE',  ( -12.29999999973083114, -29.92191803000494232, -29.18524365327784409 ) ) ;
#18189=CARTESIAN_POINT ( 'NONE',  ( -17.38746449168020902, -25.68346034424820701, -33.41339816745249891 ) ) ;
#18213=ADVANCED_FACE ( 'NONE', ( #15082 ), #17724, .T. ) ;
#18218=PLANE ( 'NONE',  #3394 ) ;
#18219=CARTESIAN_POINT ( 'NONE',  ( -17.35782682096789031, -28.15616391712504551, -23.29400885707979896 ) ) ;
#18295=CARTESIAN_POINT ( 'NONE',  ( -17.49999999932747130, -30.00000000000000000, -28.40000000020000215 ) ) ;
#18313=CARTESIAN_POINT ( 'NONE',  ( -17.32507820269023924, -22.93869108212583185, -24.97139291864791488 ) ) ;
#18318=DIRECTION ( 'NONE',  ( -1.000000000000000000, 0.000000000000000000, 0.000000000000000000 ) ) ;
#18328=CARTESIAN_POINT ( 'NONE',  ( -17.49199711315135986, -24.60220466956999985, -24.01086508779000184 ) ) ;
#18360=CARTESIAN_POINT ( 'NONE',  ( -12.59531001298596387, -22.00000000000000355, -30.73779220032784210 ) ) ;
#18362=CARTESIAN_POINT ( 'NONE',  ( -17.12355120911344741, -21.99999999999975842, -25.78113483056816690 ) ) ;
#18392=CARTESIAN_POINT ( 'NONE',  ( -17.49999999969999820, -27.00000000000000000, -28.40000000020000215 ) ) ;
#18406=DIRECTION ( 'NONE',  ( 1.000000000000000000, 0.000000000000000000, 0.000000000000000000 ) ) ;
#18469=CARTESIAN_POINT ( 'NONE',  ( -17.42785659857125324, -23.57399342402652920, -24.60449948155520516 ) ) ;
#18542=CARTESIAN_POINT ( 'NONE',  ( -17.40775135787899686, -30.56179203344806083, -24.68289889760973210 ) ) ;
#18729=AXIS2_PLACEMENT_3D ( 'NONE', #26463, #16395, #4906 ) ;
#18782=ORIENTED_EDGE ( 'NONE', *, *, #20537, .F. ) ;
#18799=EDGE_CURVE ( 'NONE', #8301, #16868, #25761, .T. ) ;
#18842=DIRECTION ( 'NONE',  ( 1.000000000000000000, 0.000000000000000000, 0.000000000000000000 ) ) ;
#18848=CARTESIAN_POINT ( 'NONE',  ( -17.48838570233685275, -29.74446036096981771, -32.58900154053760900 ) ) ;
#18927=CARTESIAN_POINT ( 'NONE',  ( -17.49999999969999465, -27.78076054102322345, -31.32371301078582704 ) ) ;
#18972=CARTESIAN_POINT ( 'NONE',  ( -17.31982526421443680, -22.92225716952031078, -31.81921677123528980 ) ) ;
#18982=CARTESIAN_POINT ( 'NONE',  ( -12.37231291231705832, -30.42659210113913915, -32.19515882010285424 ) ) ;
#18988=CARTESIAN_POINT ( 'NONE',  ( -14.90000000006999947, -30.00000000000000000, -28.40000000020000215 ) ) ;
#19072=EDGE_CURVE ( 'NONE', #17371, #11184, #30612, .T. ) ;
#19085=CLOSED_SHELL ( 'NONE', ( #14315, #24603, #24786, #10735, #26414, #28479, #24834, #4266, #22128, #18213, #17702, #11666, #23080, #5898 ) ) ;
#19143=CARTESIAN_POINT ( 'NONE',  ( -12.58977862431063244, -31.50799326805841361, -31.57081156527973675 ) ) ;
#19154=CARTESIAN_POINT ( 'NONE',  ( -17.04621913067799710, -22.00000000000000000, -25.51324865357000249 ) ) ;
#19155=ORIENTED_EDGE ( 'NONE', *, *, #13270, .F. ) ;
#19229=CARTESIAN_POINT ( 'NONE',  ( -12.34127026248727077, -32.00000000000001421, -29.28730138128909033 ) ) ;
#19324=CARTESIAN_POINT ( 'NONE',  ( -17.48914026050863768, -24.78381054247710225, -23.90601488817711839 ) ) ;
#19389=CARTESIAN_POINT ( 'NONE',  ( -12.40011512277772354, -32.00000000000000000, -27.11758776248545999 ) ) ;
#19398=CARTESIAN_POINT ( 'NONE',  ( -17.49999999969999820, -24.00000000000000000, -28.40000000020000215 ) ) ;
#19406=CARTESIAN_POINT ( 'NONE',  ( -17.37426278433457583, -31.99976580709003926, -29.84888108430074638 ) ) ;
#19441=PRODUCT_DEFINITION_CONTEXT ( 'detailed design', #29691, 'design' ) ;
#19523=CARTESIAN_POINT ( 'NONE',  ( -12.59914306489253200, -31.53608658979329604, -25.24540812198844364 ) ) ;
#19552=ORIENTED_EDGE ( 'NONE', *, *, #11697, .F. ) ;
#19570=CARTESIAN_POINT ( 'NONE',  ( -12.41634270791311323, -28.29799050060249854, -33.42410161962300208 ) ) ;
#19601=CARTESIAN_POINT ( 'NONE',  ( -17.41896590621361085, -22.00022434743734578, -29.54135749160853663 ) ) ;
#19645=CARTESIAN_POINT ( 'NONE',  ( -12.42573721507907081, -25.75488492242208594, -33.45436474419933148 ) ) ;
#19697=CARTESIAN_POINT ( 'NONE',  ( -12.40388755362273798, -32.00000000000000000, -27.09135028366836906 ) ) ;
#19826=ORIENTED_EDGE ( 'NONE', *, *, #9649, .T. ) ;
#19839=AXIS2_PLACEMENT_3D ( 'NONE', #28044, #16089, #25701 ) ;
#19893=CARTESIAN_POINT ( 'NONE',  ( -12.30800288698999978, -24.60220466956999985, -24.01086508779000184 ) ) ;
#19938=EDGE_CURVE ( 'NONE', #11502, #4065, #26083, .T. ) ;
#19941=FACE_OUTER_BOUND ( 'NONE', #11152, .T. ) ;
#19949=CARTESIAN_POINT ( 'NONE',  ( -12.40047914202865620, -23.38968038405745276, -32.08884053860782615 ) ) ;
#19987=DIRECTION ( 'NONE',  ( 0.000000000000000000, -1.000000000000000000, 0.000000000000000000 ) ) ;
#19993=CARTESIAN_POINT ( 'NONE',  ( -17.04621913067799710, -27.00000000000000355, -34.17350269210000135 ) ) ;
#20015=DIRECTION ( 'NONE',  ( 0.4999999999969509945, 0.4151946956549595336, 0.7600087925169251024 ) ) ;
#20036=CARTESIAN_POINT ( 'NONE',  ( -12.36045835447018248, -25.34141119637459738, -23.58428766072654525 ) ) ;
#20046=FILL_AREA_STYLE ('',( #27128 ) ) ;
#20050=CARTESIAN_POINT ( 'NONE',  ( -12.75378086759999796, -32.00000000058999916, -25.51324865459000080 ) ) ;
#20101=CARTESIAN_POINT ( 'NONE',  ( -12.29999999985416892, -27.78524365307783839, -31.32191803020494802 ) ) ;
#20110=CARTESIAN_POINT ( 'NONE',  ( -12.52275726677833134, -26.20837313925740730, -33.71604460516739010 ) ) ;
#20174=CIRCLE ( 'NONE', #30213, 2.999999999999999112 ) ;
#20239=CARTESIAN_POINT ( 'NONE',  ( -12.29999999994666382, -25.48914305888729714, -31.02135916526277271 ) ) ;
#20241=CARTESIAN_POINT ( 'NONE',  ( -17.38249745079132680, -25.71151397014635975, -33.42959493591655473 ) ) ;
#20316=CARTESIAN_POINT ( 'NONE',  ( -17.04621913067799710, -32.00000000000000000, -31.28675134614999820 ) ) ;
#20348=EDGE_CURVE ( 'NONE', #9043, #7844, #11571, .T. ) ;
#20404=CARTESIAN_POINT ( 'NONE',  ( -17.41915764887747997, -23.51136720943065228, -32.15933961136000363 ) ) ;
#20537=EDGE_CURVE ( 'NONE', #2751, #16868, #26294, .T. ) ;
#20558=CARTESIAN_POINT ( 'NONE',  ( -12.30000000000833005, -24.37864083493721878, -29.91085694131269790 ) ) ;
#20607=CARTESIAN_POINT ( 'NONE',  ( -17.38583936187866996, -28.31016903684225738, -33.41707624599442994 ) ) ;
#20626=SHAPE_REPRESENTATION ( 'Nut M6', ( #17722 ), #23366 ) ;
#20673=ORIENTED_EDGE ( 'NONE', *, *, #3522, .F. ) ;
#20701=EDGE_CURVE ( 'NONE', #14380, #4065, #20174, .T. ) ;
#20721=CARTESIAN_POINT ( 'NONE',  ( -12.34127026248313364, -22.00000000000000711, -27.51269861918589044 ) ) ;
#20809=MANIFOLD_SOLID_BREP ( 'PartBody', #19085 ) ;
#20833=DIRECTION ( 'NONE',  ( 0.000000000000000000, 1.000000000000000000, 0.000000000000000000 ) ) ;
#20913=ORIENTED_EDGE ( 'NONE', *, *, #2907, .T. ) ;
#20929=CARTESIAN_POINT ( 'NONE',  ( -14.89999999913999851, -27.00000000059169736, -22.62649730796000114 ) ) ;
#20995=CARTESIAN_POINT ( 'NONE',  ( -17.43796590507927746, -23.65055572458717492, -24.56029040692275345 ) ) ;
#21072=CARTESIAN_POINT ( 'NONE',  ( -17.37283180966073459, -28.23568901534668285, -23.33992269394541452 ) ) ;
#21167=DIRECTION ( 'NONE',  ( -0.4999999999969509945, 0.4151946956549595336, 0.7600087925169251024 ) ) ;
#21213=CARTESIAN_POINT ( 'NONE',  ( -17.49355845095107043, -29.49704728436632806, -32.73183177029086011 ) ) ;
#21475=ORIENTED_EDGE ( 'NONE', *, *, #2907, .F. ) ;
#21476=CARTESIAN_POINT ( 'NONE',  ( -12.38365826780663426, -23.49682068899581466, -24.64905882652923097 ) ) ;
#21577=DIRECTION ( 'NONE',  ( 1.000000000000000000, 0.000000000000000000, 0.000000000000000000 ) ) ;
#21599=CARTESIAN_POINT ( 'NONE',  ( -12.48073050767949965, -32.00000000000000000, -30.16865675522091905 ) ) ;
#21658=CARTESIAN_POINT ( 'NONE',  ( -17.20085693451147790, -21.99999999999968736, -30.75107028161901468 ) ) ;
#21687=EDGE_CURVE ( 'NONE', #24188, #14200, #1942, .T. ) ;
#21743=CARTESIAN_POINT ( 'NONE',  ( -17.49999999969999820, -22.00000000000000000, -31.28675134614999820 ) ) ;
#21759=CARTESIAN_POINT ( 'NONE',  ( -14.89999999913999851, -22.00000000000000000, -25.51324865424999899 ) ) ;
#21766=CARTESIAN_POINT ( 'NONE',  ( -17.20085693451561681, -32.00000000000027711, -26.04892971879526442 ) ) ;
#21776=CARTESIAN_POINT ( 'NONE',  ( -12.31092893605830696, -29.21179069622078117, -32.89652473824072842 ) ) ;
#21786=B_SPLINE_CURVE_WITH_KNOTS ( 'NONE', 3,
 ( #6198, #28221, #25723, #4158, #13277, #1958, #3845, #1492, #11236, #20995, #18469, #15635, #8707, #30598, #25411, #18313, #11086, #4316 ),
 .UNSPECIFIED., .F., .F.,
 ( 4, 2, 2, 2, 2, 1, 1, 2, 2, 4 ),
 ( 0.000000000000000000, 0.1250000000000101585, 0.1875000000000161815, 0.2500000000000222045, 0.3750000000000344724, 0.4375000000000404676, 0.4687500000000434097, 0.4843750000000421885, 0.5000000000000409672, 1.000000000000000000 ),
 .UNSPECIFIED. ) ;
#21808=CARTESIAN_POINT ( 'NONE',  ( -17.38167868480947931, -22.00021832957186163, -26.99851627150150080 ) ) ;
#21816=CARTESIAN_POINT ( 'NONE',  ( -12.30800288698999978, -29.39779533043000015, -32.78913491261000246 ) ) ;
#21904=( NAMED_UNIT ( * ) SI_UNIT ( $, .STERADIAN. ) SOLID_ANGLE_UNIT ( ) );
#21912=EDGE_CURVE ( 'NONE', #24188, #1475, #1551, .T. ) ;
#21930=CARTESIAN_POINT ( 'NONE',  ( -17.48420900742980422, -31.99983740011833788, -27.95389062477287823 ) ) ;
#21968=CARTESIAN_POINT ( 'NONE',  ( -17.45889703378724178, -22.00009059174836423, -27.51494980511629507 ) ) ;
#22045=CARTESIAN_POINT ( 'NONE',  ( -12.75378086759999796, -32.00000000058999916, -25.51324865459000080 ) ) ;
#22080=CARTESIAN_POINT ( 'NONE',  ( -17.33922399257544456, -31.99968944003585136, -30.05453958706431195 ) ) ;
#22082=EDGE_LOOP ( 'NONE', ( #3980, #14308, #28986, #14162, #8000, #1122 ) ) ;
#22088=CARTESIAN_POINT ( 'NONE',  ( -12.49429647968976198, -27.86501451498057946, -33.67401726951144525 ) ) ;
#22098=CARTESIAN_POINT ( 'NONE',  ( -12.41448843475970065, -25.69155578914772775, -23.38193380457397552 ) ) ;
#22128=ADVANCED_FACE ( 'NONE', ( #1623 ), #28879, .T. ) ;
#22140=ORIENTED_EDGE ( 'NONE', *, *, #9513, .T. ) ;
#22160=CARTESIAN_POINT ( 'NONE',  ( -12.60902638015870281, -26.54211788905850611, -33.90886144134552183 ) ) ;
#22231=CARTESIAN_POINT ( 'NONE',  ( -17.45889703378360025, -31.99990940826297958, -29.28505019524934738 ) ) ;
#22303=CARTESIAN_POINT ( 'NONE',  ( -12.29999999982333492, -28.51085694111270286, -31.02135916526277981 ) ) ;
#22344=CARTESIAN_POINT ( 'NONE',  ( -12.46077600684266962, -28.06697140616160269, -23.24287214062465523 ) ) ;
#22350=DIRECTION ( 'NONE',  ( -0.4999999999969509945, -0.4151946956549595336, -0.7600087925169251024 ) ) ;
#22511=VECTOR ( 'NONE', #4465, 1000.000000000000000 ) ;
#22618=CARTESIAN_POINT ( 'NONE',  ( -17.12540385515260866, -26.76244582786289072, -34.03635072686944341 ) ) ;
#22664=DIRECTION ( 'NONE',  ( -1.000000000000000000, 0.000000000000000000, 0.000000000000000000 ) ) ;
#22669=VECTOR ( 'NONE', #21167, 1000.000000000000227 ) ;
#22755=EDGE_LOOP ( 'NONE', ( #28583, #4431 ) ) ;
#22798=VERTEX_POINT ( 'NONE', #11067 ) ;
#22907=PRODUCT_DEFINITION_FORMATION_WITH_SPECIFIED_SOURCE ( 'ANY', '', #3799, .NOT_KNOWN. ) ;
#22931=CARTESIAN_POINT ( 'NONE',  ( -12.41253550772600889, -21.99999999999999645, -27.03345770352192545 ) ) ;
#22962=LINE ( 'NONE', #3594, #16458 ) ;
#23080=ADVANCED_FACE ( 'NONE', ( #363 ), #5522, .F. ) ;
#23271=CARTESIAN_POINT ( 'NONE',  ( -17.48108435972729424, -29.89324280579608839, -32.50314025840578580 ) ) ;
#23332=CARTESIAN_POINT ( 'NONE',  ( -12.30000000006999805, -27.00000000000000000, -28.40000000020000215 ) ) ;
#23366=( GEOMETRIC_REPRESENTATION_CONTEXT ( 3 ) GLOBAL_UNCERTAINTY_ASSIGNED_CONTEXT ( ( #16918 ) ) GLOBAL_UNIT_ASSIGNED_CONTEXT ( ( #29643, #1159, #1013 ) ) REPRESENTATION_CONTEXT ( 'NONE', 'WORKASPACE' ) );
#23369=ORIENTED_EDGE ( 'NONE', *, *, #25559, .F. ) ;
#23410=CARTESIAN_POINT ( 'NONE',  ( -12.35698168758715099, -22.00000000000000000, -29.34490690764078380 ) ) ;
#23443=CARTESIAN_POINT ( 'NONE',  ( -17.20468998641199576, -31.52458743410349484, -25.23876908135297015 ) ) ;
#23567=CARTESIAN_POINT ( 'NONE',  ( -12.44217317843894222, -22.00000000000000355, -26.84827175176876324 ) ) ;
#23586=AXIS2_PLACEMENT_3D ( 'NONE', #27965, #1068, #3894 ) ;
#23596=CARTESIAN_POINT ( 'NONE',  ( -17.04621913067799710, -27.00000000059169736, -22.62649730796000114 ) ) ;
#23679=DIRECTION ( 'NONE',  ( 0.000000000000000000, 1.000000000000000000, 0.000000000000000000 ) ) ;
#23839=CARTESIAN_POINT ( 'NONE',  ( -12.30800288698999978, -29.39779533043000015, -32.78913491261000246 ) ) ;
#23882=AXIS2_PLACEMENT_3D ( 'NONE', #3722, #13319, #10966 ) ;
#23927=ORIENTED_EDGE ( 'NONE', *, *, #15574, .F. ) ;
#23943=CARTESIAN_POINT ( 'NONE',  ( -14.89999999913999851, -32.00000000000000000, -31.28675134683000536 ) ) ;
#23958=( NAMED_UNIT ( * ) PLANE_ANGLE_UNIT ( ) SI_UNIT ( $, .RADIAN. ) );
#24047=CARTESIAN_POINT ( 'NONE',  ( -17.40937546595008101, -25.54985367907119453, -23.46373967705341457 ) ) ;
#24060=VERTEX_POINT ( 'NONE', #31071 ) ;
#24114=CARTESIAN_POINT ( 'NONE',  ( -12.30772508779320695, -31.99999999999999289, -28.84027805903673780 ) ) ;
#24129=CARTESIAN_POINT ( 'NONE',  ( -17.31586207618096651, -31.99964831253470621, -26.55600617737724534 ) ) ;
#24166=CARTESIAN_POINT ( 'NONE',  ( -17.49266624248041779, -21.99978574281297483, -28.62488781290136686 ) ) ;
#24188=VERTEX_POINT ( 'NONE', #1977 ) ;
#24221=ORIENTED_EDGE ( 'NONE', *, *, #21687, .F. ) ;
#24246=CARTESIAN_POINT ( 'NONE',  ( -12.75378086759999796, -22.00000000000000000, -31.28675134614999820 ) ) ;
#24260=DIRECTION ( 'NONE',  ( 1.000000000000000000, 0.000000000000000000, 0.000000000000000000 ) ) ;
#24320=CARTESIAN_POINT ( 'NONE',  ( -17.38654519918314278, -22.00020860527460798, -27.03011121754735413 ) ) ;
#24353=CARTESIAN_POINT ( 'NONE',  ( -17.38968115014047200, -25.66781448189618331, -23.39563497578856399 ) ) ;
#24380=B_SPLINE_CURVE_WITH_KNOTS ( 'NONE', 3,
 ( #296, #19324, #26852, #29209, #24047, #28750, #24353, #7203, #7359, #2793, #7654 ),
 .UNSPECIFIED., .F., .F.,
 ( 4, 1, 1, 1, 2, 2, 4 ),
 ( 0.000000000000000000, 0.2499999999999976130, 0.3749999999999972244, 0.4374999999999980571, 0.4687499999999981681, 0.4999999999999983347, 1.000000000000000000 ),
 .UNSPECIFIED. ) ;
#24400=CARTESIAN_POINT ( 'NONE',  ( -12.35171651922531666, -30.27052668731191432, -24.51507340929063616 ) ) ;
#24438=CARTESIAN_POINT ( 'NONE',  ( -17.35614611410398211, -31.99972351093158807, -29.95953050019675246 ) ) ;
#24502=B_SPLINE_CURVE_WITH_KNOTS ( 'NONE', 3,
 ( #30321, #18362, #27958, #7482, #14886, #2606, #16920, #15038, #21808, #24320, #14420, #21968, #265, #24166, #12200, #26830, #28885, #29182, #19601, #29036, #12359, #26527, #5427, #17076, #21658, #7629 ),
 .UNSPECIFIED., .F., .F.,
 ( 4, 2, 2, 1, 1, 2, 2, 2, 2, 2, 1, 1, 2, 2, 4 ),
 ( 0.000000000000000000, 0.1249999999999961142, 0.1874999999999943379, 0.2187499999999933109, 0.2343749999999934774, 0.2421874999999935885, 0.2499999999999936717, 0.4999999999999868994, 0.6249999999999825695, 0.6874999999999803491, 0.7187499999999782396, 0.7343749999999771294, 0.7421874999999775735, 0.7499999999999780176, 1.000000000000000000 ),
 .UNSPECIFIED. ) ;
#24522=CARTESIAN_POINT ( 'NONE',  ( -12.35171651922521718, -23.72947331268410309, -32.28492659110577279 ) ) ;
#24552=CARTESIAN_POINT ( 'NONE',  ( -12.48413792322954308, -31.09676965128281978, -24.99217446298782619 ) ) ;
#24573=VECTOR ( 'NONE', #5923, 1000.000000000000000 ) ;
#24603=ADVANCED_FACE ( 'NONE', ( #2397 ), #29125, .T. ) ;
#24610=CARTESIAN_POINT ( 'NONE',  ( -12.34929264640405577, -25.24897882093459245, -23.63770812723453574 ) ) ;
#24648=VERTEX_POINT ( 'NONE', #16859 ) ;
#24711=CARTESIAN_POINT ( 'NONE',  ( -17.49999999969999820, -32.00000000000000000, -25.51324865424999899 ) ) ;
#24720=VECTOR ( 'NONE', #1491, 1000.000000000000227 ) ;
#24786=ADVANCED_FACE ( 'NONE', ( #7869 ), #29590, .T. ) ;
#24813=AXIS2_PLACEMENT_3D ( 'NONE', #2330, #26696, #9392 ) ;
#24822=CARTESIAN_POINT ( 'NONE',  ( -14.89999999913999851, -26.99999999940830264, -34.17350269244000316 ) ) ;
#24829=CARTESIAN_POINT ( 'NONE',  ( -12.37073348361115954, -23.58440183081340535, -32.20121653530289763 ) ) ;
#24834=ADVANCED_FACE ( 'NONE', ( #11021 ), #4242, .T. ) ;
#24967=CARTESIAN_POINT ( 'NONE',  ( -12.29999999990041459, -26.60730091830127009, -31.40000000019999860 ) ) ;
#24969=CARTESIAN_POINT ( 'NONE',  ( -17.37283180965889784, -25.76431098467556424, -33.46007730646741152 ) ) ;
#25006=CARTESIAN_POINT ( 'NONE',  ( -12.41081696006088819, -28.32863187924899862, -23.39381857568974965 ) ) ;
#25126=CARTESIAN_POINT ( 'NONE',  ( -17.47972357343276428, -24.02078344067320970, -32.45345120959760976 ) ) ;
#25286=CARTESIAN_POINT ( 'NONE',  ( -12.67459614424639902, -22.00000000000000355, -25.78755258470928524 ) ) ;
#25298=AXIS2_PLACEMENT_3D ( 'NONE', #5163, #16816, #12710 ) ;
#25319=CARTESIAN_POINT ( 'NONE',  ( -12.29999999969999891, -27.00000000000000000, -28.40000000020000215 ) ) ;
#25365=AXIS2_PLACEMENT_3D ( 'NONE', #24711, #19987, #5509 ) ;
#25411=CARTESIAN_POINT ( 'NONE',  ( -17.40256142130785832, -23.40875500259708986, -24.69991345770832680 ) ) ;
#25437=CARTESIAN_POINT ( 'NONE',  ( -12.75378086759999796, -27.00000000059169736, -22.62649730796000114 ) ) ;
#25451=CARTESIAN_POINT ( 'NONE',  ( -12.39224864152920880, -22.00000000000000000, -29.62605183290172306 ) ) ;
#25479=FACE_OUTER_BOUND ( 'NONE', #30618, .T. ) ;
#25556=CARTESIAN_POINT ( 'NONE',  ( -12.29999999969999891, -27.00000000000000000, -28.40000000020000215 ) ) ;
#25559=EDGE_CURVE ( 'NONE', #11184, #1865, #2129, .T. ) ;
#25561=CARTESIAN_POINT ( 'NONE',  ( -250010.8602219996974, 207571.5434020000394, 379978.1847439997364 ) ) ;
#25701=DIRECTION ( 'NONE',  ( 0.000000000000000000, 0.4794255386042043932, 0.8775825618903719816 ) ) ;
#25723=CARTESIAN_POINT ( 'NONE',  ( -17.49285076559437613, -24.40406112000763628, -24.12527371869715864 ) ) ;
#25761=B_SPLINE_CURVE_WITH_KNOTS ( 'NONE', 3,
 ( #27184, #5469, #22160, #20110, #12703, #15223, #10049, #19645, #29387, #765, #26880, #27339, #7668, #17577, #5321, #14925, #24522, #24829, #10202, #10358, #19949, #12553, #29542, #8124, #3261, #17426 ),
 .UNSPECIFIED., .F., .F.,
 ( 4, 2, 2, 1, 1, 2, 2, 2, 2, 2, 1, 1, 2, 2, 4 ),
 ( 0.000000000000000000, 0.1249999999999994449, 0.1875000000000006661, 0.2187500000000019151, 0.2343750000000026090, 0.2421875000000029698, 0.2500000000000033307, 0.4999999999999833467, 0.6249999999999734657, 0.6874999999999695799, 0.7187499999999664713, 0.7343749999999659162, 0.7421874999999655831, 0.7499999999999653610, 1.000000000000000000 ),
 .UNSPECIFIED. ) ;
#25763=CARTESIAN_POINT ( 'NONE',  ( -12.48073050767821002, -22.00000000000000000, -26.63134324521094598 ) ) ;
#25788=PRODUCT_CONTEXT ( 'NONE', #2139, 'mechanical' ) ;
#25795=CARTESIAN_POINT ( 'NONE',  ( -17.31926949172702024, -27.96829831963164636, -23.18554460379546711 ) ) ;
#25855=ORIENTED_EDGE ( 'NONE', *, *, #18113, .F. ) ;
#25966=CARTESIAN_POINT ( 'NONE',  ( -17.49999999965344344, -27.00000000000000000, -28.40000000020000215 ) ) ;
#26016=ORIENTED_EDGE ( 'NONE', *, *, #7747, .T. ) ;
#26049=CARTESIAN_POINT ( 'NONE',  ( -12.58977862431605388, -22.49200673191992550, -25.22918843513278375 ) ) ;
#26083=LINE ( 'NONE', #18988, #71 ) ;
#26089=ADVANCED_BREP_SHAPE_REPRESENTATION ( '', ( #20809, #17722 ), #23366 ) ;
#26098=CARTESIAN_POINT ( 'NONE',  ( -17.40850972538804697, -30.55410961813850790, -32.12153152511883292 ) ) ;
#26206=MECHANICAL_DESIGN_GEOMETRIC_PRESENTATION_REPRESENTATION('',(#30719),#9095);
#26294=LINE ( 'NONE', #16684, #12110 ) ;
#26325=ORIENTED_EDGE ( 'NONE', *, *, #19938, .F. ) ;
#26326=CARTESIAN_POINT ( 'NONE',  ( -17.49999999969999820, -26.21905350739292473, -31.32349012542221089 ) ) ;
#26404=ORIENTED_EDGE ( 'NONE', *, *, #10942, .F. ) ;
#26414=ADVANCED_FACE ( 'NONE', ( #26547 ), #28600, .T. ) ;
#26463=CARTESIAN_POINT ( 'NONE',  ( -17.49999999969999820, -27.00000000000000000, -28.40000000020000215 ) ) ;
#26477=CARTESIAN_POINT ( 'NONE',  ( -17.49999999969999820, -30.00000000000000000, -28.79765167477413357 ) ) ;
#26486=VERTEX_POINT ( 'NONE', #19154 ) ;
#26494=CARTESIAN_POINT ( 'NONE',  ( -12.41036288881528016, -28.33197836327668639, -33.40447669382125895 ) ) ;
#26502=CARTESIAN_POINT ( 'NONE',  ( -12.31403527401453424, -24.10534946231254239, -24.29772457544500597 ) ) ;
#26527=CARTESIAN_POINT ( 'NONE',  ( -17.39542721469608821, -22.00021333527590883, -29.71046973867640872 ) ) ;
#26547=FACE_OUTER_BOUND ( 'NONE', #29130, .T. ) ;
#26630=ORIENTED_EDGE ( 'NONE', *, *, #13270, .T. ) ;
#26634=LINE ( 'NONE', #6977, #22511 ) ;
#26696=DIRECTION ( 'NONE',  ( 0.000000000000000000, -0.5000000000001900702, -0.8660254037843290176 ) ) ;
#26763=SURFACE_STYLE_FILL_AREA ( #7412 ) ;
#26771=CARTESIAN_POINT ( 'NONE',  ( -12.42716818975153892, -32.00000000000000711, -29.85990057496828953 ) ) ;
#26783=CARTESIAN_POINT ( 'NONE',  ( -17.49999999932747130, -30.00000000000000000, -28.40000000020000215 ) ) ;
#26830=CARTESIAN_POINT ( 'NONE',  ( -17.45884911674703588, -22.00029789592859686, -29.17883862680921681 ) ) ;
#26852=CARTESIAN_POINT ( 'NONE',  ( -17.47315945020447359, -25.05913013249180565, -23.74705904876886109 ) ) ;
#26874=( GEOMETRIC_REPRESENTATION_CONTEXT ( 3 ) GLOBAL_UNCERTAINTY_ASSIGNED_CONTEXT ( ( #14418 ) ) GLOBAL_UNIT_ASSIGNED_CONTEXT ( ( #17974, #27587, #13265 ) ) REPRESENTATION_CONTEXT ( 'NONE', 'WORKASPACE' ) );
#26880=CARTESIAN_POINT ( 'NONE',  ( -12.41081696005857715, -25.67136812075533925, -33.40618142470727747 ) ) ;
#26951=CARTESIAN_POINT ( 'NONE',  ( -17.41896590622109287, -31.99977565255875689, -27.25864250883248374 ) ) ;
#26957=CARTESIAN_POINT ( 'NONE',  ( -12.40426553250898500, -28.36724026820617794, -33.38411139160245256 ) ) ;
#27128=FILL_AREA_STYLE_COLOUR ( '', #9252 ) ;
#27176=CARTESIAN_POINT ( 'NONE',  ( -17.04621913067799710, -27.00000000000000355, -34.17350269210000135 ) ) ;
#27184=CARTESIAN_POINT ( 'NONE',  ( -12.75378086759999796, -27.00000000000000355, -34.17350269210000135 ) ) ;
#27339=CARTESIAN_POINT ( 'NONE',  ( -12.34110296562673881, -25.26652124847552017, -33.17257366193984325 ) ) ;
#27423=ORIENTED_EDGE ( 'NONE', *, *, #10636, .F. ) ;
#27453=ORIENTED_EDGE ( 'NONE', *, *, #13004, .T. ) ;
#27472=CARTESIAN_POINT ( 'NONE',  ( -12.30000000006999805, -24.00000000000000000, -28.40000000020000215 ) ) ;
#27587=( NAMED_UNIT ( * ) PLANE_ANGLE_UNIT ( ) SI_UNIT ( $, .RADIAN. ) );
#27617=B_SPLINE_CURVE_WITH_KNOTS ( 'NONE', 3,
 ( #23596, #18061, #16027, #25795, #18219, #21072, #10848, #4230, #13670, #30357, #13510, #1566, #13830, #27827, #18542, #8944, #6430, #1719, #23443, #30032 ),
 .UNSPECIFIED., .F., .F.,
 ( 4, 1, 1, 1, 2, 2, 2, 1, 1, 1, 2, 2, 4 ),
 ( 0.000000000000000000, 0.1250000000000007494, 0.1875000000000013600, 0.2187500000000012212, 0.2343750000000005829, 0.2499999999999999167, 0.5000000000000047740, 0.6250000000000075495, 0.6875000000000081046, 0.7187500000000083267, 0.7343750000000085487, 0.7500000000000087708, 1.000000000000000000 ),
 .UNSPECIFIED. ) ;
#27681=CARTESIAN_POINT ( 'NONE',  ( -17.30852986267844429, -27.88015086496476158, -33.66534735328443873 ) ) ;
#27783=ORIENTED_EDGE ( 'NONE', *, *, #18799, .T. ) ;
#27796=ORIENTED_EDGE ( 'NONE', *, *, #19072, .F. ) ;
#27826=CARTESIAN_POINT ( 'NONE',  ( -12.29999999969999891, -27.00000000000000000, -28.40000000020000215 ) ) ;
#27827=CARTESIAN_POINT ( 'NONE',  ( -17.41915764888113216, -30.48863279055043662, -24.64066038902905831 ) ) ;
#27958=CARTESIAN_POINT ( 'NONE',  ( -17.19097361924276868, -22.00024499056281613, -26.04210681964482887 ) ) ;
#27965=CARTESIAN_POINT ( 'NONE',  ( -17.49999999969999820, -27.00000000000000355, -34.17350269210000135 ) ) ;
#28044=CARTESIAN_POINT ( 'NONE',  ( -12.29999999974999803, -27.00000000000000000, -28.40000000020000215 ) ) ;
#28160=CARTESIAN_POINT ( 'NONE',  ( -17.40937546593514895, -28.45014632087456619, -33.33626032337789269 ) ) ;
#28221=CARTESIAN_POINT ( 'NONE',  ( -17.49355845095121609, -24.50295271566449529, -24.06816823009259210 ) ) ;
#28261=CARTESIAN_POINT ( 'NONE',  ( -17.20468998641224800, -22.47541256591814474, -31.56123091905952549 ) ) ;
#28262=CARTESIAN_POINT ( 'NONE',  ( -12.40011512277526862, -21.99999999999999289, -29.68241223786358773 ) ) ;
#28407=CIRCLE ( 'NONE', #8781, 4.987531172950001590 ) ;
#28448=CARTESIAN_POINT ( 'NONE',  ( -17.48633009204728239, -29.79399746876627120, -32.56041429237782125 ) ) ;
#28479=ADVANCED_FACE ( 'NONE', ( #3604 ), #13200, .T. ) ;
#28496=DIRECTION ( 'NONE',  ( 1.000000000000000000, 0.000000000000000000, 0.000000000000000000 ) ) ;
#28525=CARTESIAN_POINT ( 'NONE',  ( -17.49999999969999820, -24.59808825516011410, -30.23948587685871559 ) ) ;
#28583=ORIENTED_EDGE ( 'NONE', *, *, #8017, .T. ) ;
#28600=PLANE ( 'NONE',  #24813 ) ;
#28680=CARTESIAN_POINT ( 'NONE',  ( -17.49999999969999820, -29.92349012522117846, -29.18094649280867614 ) ) ;
#28750=CARTESIAN_POINT ( 'NONE',  ( -17.39770507061216165, -25.62059377601494603, -23.42289786304042920 ) ) ;
#28877=AXIS2_PLACEMENT_3D ( 'NONE', #13058, #3306, #22664 ) ;
#28879=CONICAL_SURFACE ( 'NONE', #19839, 4.987531172069999741, 1.047197551199999799 ) ;
#28885=CARTESIAN_POINT ( 'NONE',  ( -17.44828348017237829, -22.00029153676899440, -29.28989589971321195 ) ) ;
#28903=AXIS2_PLACEMENT_3D ( 'NONE', #666, #24260, #15126 ) ;
#28910=ORIENTED_EDGE ( 'NONE', *, *, #7747, .F. ) ;
#28979=CARTESIAN_POINT ( 'NONE',  ( -12.75378086759999796, -32.00000000000000000, -31.28675134614999820 ) ) ;
#28986=ORIENTED_EDGE ( 'NONE', *, *, #18113, .T. ) ;
#28994=CARTESIAN_POINT ( 'NONE',  ( -17.38167868481496114, -31.99978167043220623, -29.80148372884886498 ) ) ;
#29036=CARTESIAN_POINT ( 'NONE',  ( -17.40556230546145500, -22.00020956758401525, -29.63986184916237221 ) ) ;
#29125=PLANE ( 'NONE',  #13283 ) ;
#29128=CARTESIAN_POINT ( 'NONE',  ( -12.57202792198531682, -32.00000000000000000, -30.61316950642639867 ) ) ;
#29130=EDGE_LOOP ( 'NONE', ( #1219, #8110, #27453, #12900, #3118, #15905 ) ) ;
#29146=CARTESIAN_POINT ( 'NONE',  ( -17.30352168679151248, -31.99964266802675894, -30.24496221943030250 ) ) ;
#29163=CARTESIAN_POINT ( 'NONE',  ( -12.40426553248159180, -25.63275973170342326, -23.41588860887158319 ) ) ;
#29182=CARTESIAN_POINT ( 'NONE',  ( -17.42926651578709496, -22.00025083071089682, -29.45738651627399918 ) ) ;
#29203=DIRECTION ( 'NONE',  ( 1.000000000000000000, 0.000000000000000000, 0.000000000000000000 ) ) ;
#29208=ORIENTED_EDGE ( 'NONE', *, *, #2519, .T. ) ;
#29209=CARTESIAN_POINT ( 'NONE',  ( -17.43404799081794465, -25.38543018601581736, -23.55866962503008821 ) ) ;
#29258=CARTESIAN_POINT ( 'NONE',  ( -12.42573721508254714, -28.24511507758019135, -23.34563525619502755 ) ) ;
#29282=VERTEX_POINT ( 'NONE', #19993 ) ;
#29321=ORIENTED_EDGE ( 'NONE', *, *, #3926, .T. ) ;
#29387=CARTESIAN_POINT ( 'NONE',  ( -12.41832131459880273, -25.71382967685944365, -33.43067980453216137 ) ) ;
#29530=AXIS2_PLACEMENT_3D ( 'NONE', #25556, #11227, #20833 ) ;
#29542=CARTESIAN_POINT ( 'NONE',  ( -12.40641005330448898, -23.35436477320368454, -32.06844556927040912 ) ) ;
#29569=DIRECTION ( 'NONE',  ( 1.000000000000000000, 0.000000000000000000, 0.000000000000000000 ) ) ;
#29572=CARTESIAN_POINT ( 'NONE',  ( -12.52275726678476175, -27.79162686073846444, -23.08395539522074102 ) ) ;
#29590=PLANE ( 'NONE',  #28877 ) ;
#29643=( LENGTH_UNIT ( ) NAMED_UNIT ( * ) SI_UNIT ( .MILLI., .METRE. ) );
#29690=CARTESIAN_POINT ( 'NONE',  ( -17.35782682096630225, -25.84383608289461520, -33.50599114333153494 ) ) ;
#29691=APPLICATION_CONTEXT ( 'automotive_design' ) ;
#29759=LINE ( 'NONE', #3171, #2876 ) ;
#29762=CARTESIAN_POINT ( 'NONE',  ( -17.49999999969999820, -29.39114981890000067, -32.77697038446999755 ) ) ;
#29837=CARTESIAN_POINT ( 'NONE',  ( -12.30000000003916938, -24.07808196999506123, -29.18524365327784409 ) ) ;
#29885=CARTESIAN_POINT ( 'NONE',  ( 249981.0602220003202, 207571.5434020000394, 379978.1847439997364 ) ) ;
#29992=CARTESIAN_POINT ( 'NONE',  ( -12.75378086759999796, -22.00000000000000000, -31.28675134614999820 ) ) ;
#30025=B_SPLINE_CURVE_WITH_KNOTS ( 'NONE', 3,
 ( #2724, #683, #536, #9645, #29146, #22080, #24438, #19406, #28994, #2873, #12320, #22231, #16717, #17347, #21930, #14995, #12465, #5079, #26951, #14535, #377, #12619, #17038, #24129, #21766, #4783 ),
 .UNSPECIFIED., .F., .F.,
 ( 4, 2, 2, 1, 1, 2, 2, 2, 2, 2, 1, 1, 2, 2, 4 ),
 ( 0.000000000000000000, 0.1250000000000019984, 0.1875000000000021927, 0.2187500000000021372, 0.2343750000000012768, 0.2421875000000015266, 0.2500000000000017764, 0.4999999999999836797, 0.6249999999999745759, 0.6874999999999700240, 0.7187499999999678035, 0.7343749999999679146, 0.7421874999999686917, 0.7499999999999694689, 1.000000000000000000 ),
 .UNSPECIFIED. ) ;
#30032=CARTESIAN_POINT ( 'NONE',  ( -17.04621913067799710, -32.00000000058999916, -25.51324865459000080 ) ) ;
#30047=CARTESIAN_POINT ( 'NONE',  ( -17.49199711315135986, -29.39779533043000015, -32.78913491261000246 ) ) ;
#30205=CARTESIAN_POINT ( 'NONE',  ( -17.19683899162122387, -27.45185958154430850, -33.91262144105893839 ) ) ;
#30213=AXIS2_PLACEMENT_3D ( 'NONE', #23332, #3971, #14042 ) ;
#30321=CARTESIAN_POINT ( 'NONE',  ( -17.04621913067799710, -22.00000000000000000, -25.51324865357000249 ) ) ;
#30357=CARTESIAN_POINT ( 'NONE',  ( -17.49227491161517278, -29.11870801639694406, -23.84973395190160161 ) ) ;
#30530=CARTESIAN_POINT ( 'NONE',  ( -17.43404799080784429, -28.61456981395415511, -33.24133037538724267 ) ) ;
#30578=ORIENTED_EDGE ( 'NONE', *, *, #3926, .F. ) ;
#30598=CARTESIAN_POINT ( 'NONE',  ( -17.40441589016016266, -23.42021493853068037, -24.69329539672489204 ) ) ;
#30612=B_SPLINE_CURVE_WITH_KNOTS ( 'NONE', 3,
 ( #21816, #4830, #6712, #9223, #18982, #14274, #11747, #6865, #7341, #19143, #2008 ),
 .UNSPECIFIED., .F., .F.,
 ( 4, 1, 1, 1, 2, 2, 4 ),
 ( 0.000000000000000000, 0.2500000000000190958, 0.3750000000000267564, 0.4375000000000288658, 0.4687500000000298095, 0.5000000000000307532, 1.000000000000000000 ),
 .UNSPECIFIED. ) ;
#30618=EDGE_LOOP ( 'NONE', ( #19552, #14368 ) ) ;
#30642=ORIENTED_EDGE ( 'NONE', *, *, #8473, .F. ) ;
#30704=DIRECTION ( 'NONE',  ( 1.000000000000000000, 0.000000000000000000, 0.000000000000000000 ) ) ;
#30719=STYLED_ITEM ( 'NONE', ( #350 ), #20809 ) ;
#30774=EDGE_LOOP ( 'NONE', ( #23369, #27796, #11770, #16097, #21475, #4998, #13221 ) ) ;
#30786=CARTESIAN_POINT ( 'NONE',  ( -17.40775135787469807, -23.43820796653147553, -32.11710110277844876 ) ) ;
#30923=CARTESIAN_POINT ( 'NONE',  ( -12.37231291232859043, -23.57340789884118593, -24.60484118030849032 ) ) ;
#30933=CARTESIAN_POINT ( 'NONE',  ( -17.49199711315135986, -29.39779533043000015, -32.78913491261000246 ) ) ;
#31047=CARTESIAN_POINT ( 'NONE',  ( -17.49999999969999820, -25.48537695659676672, -31.01919234699705186 ) ) ;
#31071=CARTESIAN_POINT ( 'NONE',  ( -17.04621913067799710, -32.00000000000000000, -31.28675134614999820 ) ) ;
ENDSEC;
END-ISO-10303-21;
